ISO-10303-21;
HEADER;
FILE_DESCRIPTION (('STEP AP214'),
    '1' );
FILE_NAME ('hex flange nut gradea_iso_ISO - 4161 - M8 - N.step',
    '2026-10-08T07:58:12',
    ( '' ),
    ( '' ),
    'SwSTEP 2.0',
    'SolidWorks 2026',
    '' );
FILE_SCHEMA (( 'AUTOMOTIVE_DESIGN' ));
ENDSEC;

DATA;
#40=ORIENTED_EDGE ( 'NONE', *, *, #21984, .F. ) ;
#64=CARTESIAN_POINT ( 'NONE',  ( -6.500000000000000000, -3.752776749732572803, -8.000000000000000000 ) ) ;
#65=DIRECTION ( 'NONE',  ( 0.000000000000000000, 0.000000000000000000, 1.000000000000000000 ) ) ;
#73=VERTEX_POINT ( 'NONE', #11840 ) ;
#146=CARTESIAN_POINT ( 'NONE',  ( 1.126429428730187032, -7.232124035235040438, -6.344710093416088270 ) ) ;
#152=CIRCLE ( 'NONE', #30594, 3.999999999999999112 ) ;
#237=B_SPLINE_CURVE_WITH_KNOTS ( 'NONE', 3,
 ( #14921, #6748, #30598, #12365, #7263, #16962 ),
 .UNSPECIFIED., .F., .F.,
 ( 4, 2, 4 ),
 ( 0.005511122051665409173, 0.007432374760074394321, 0.009353627468483380336 ),
 .UNSPECIFIED. ) ;
#252=CIRCLE ( 'NONE', #19276, 6.500000000000000888 ) ;
#299=EDGE_CURVE ( 'NONE', #17495, #22659, #1461, .T. ) ;
#320=VERTEX_POINT ( 'NONE', #8379 ) ;
#381=EDGE_CURVE ( 'NONE', #5932, #16641, #20514, .T. ) ;
#421=CONICAL_SURFACE ( 'NONE', #2627, 6.500000000000000888, 0.8987552595851582282 ) ;
#433=CARTESIAN_POINT ( 'NONE',  ( -6.500000000000000000, -3.752776749732572803, -6.177802698399433190 ) ) ;
#448=VECTOR ( 'NONE', #1366, 1000.000000000000000 ) ;
#495=CARTESIAN_POINT ( 'NONE',  ( -3.755786496842903988E-16, -7.505553499465146494, -8.000000000000000000 ) ) ;
#521=CARTESIAN_POINT ( 'NONE',  ( -1.860380241283027480, -6.431462466365327479, -0.1499059597315341996 ) ) ;
#531=DIRECTION ( 'NONE',  ( 0.8191520442889917986, 1.003171929053524747E-16, -0.5735764363510460484 ) ) ;
#593=CARTESIAN_POINT ( 'NONE',  ( -6.500000000000000888, -4.077972562205394169, -6.122137109124704324 ) ) ;
#615=VERTEX_POINT ( 'NONE', #21107 ) ;
#633=CARTESIAN_POINT ( 'NONE',  ( -6.781345014477444977, 3.590342129888853151, -6.122077150241850951 ) ) ;
#652=ORIENTED_EDGE ( 'NONE', *, *, #19298, .T. ) ;
#678=CARTESIAN_POINT ( 'NONE',  ( -1.604619215278546562E-14, -7.505553499465138501, -0.8000000000000003775 ) ) ;
#696=CARTESIAN_POINT ( 'NONE',  ( -6.725979247667767780, -3.622307570260316911, -6.470294263593358686 ) ) ;
#700=B_SPLINE_CURVE_WITH_KNOTS ( 'NONE', 3,
 ( #29050, #23768, #21044, #6513, #433, #21210 ),
 .UNSPECIFIED., .F., .F.,
 ( 4, 2, 4 ),
 ( -4.604908129293502741E-06, 0.0003318387708545218599, 0.0006682824498383372301 ),
 .UNSPECIFIED. ) ;
#734=VERTEX_POINT ( 'NONE', #15326 ) ;
#749=AXIS2_PLACEMENT_3D ( 'NONE', #5267, #20944, #26062 ) ;
#803=CARTESIAN_POINT ( 'NONE',  ( 6.500000000000000000, 3.752776749732573247, -0.8000000000000003775 ) ) ;
#866=VERTEX_POINT ( 'NONE', #12225 ) ;
#883=CARTESIAN_POINT ( 'NONE',  ( -3.249999999999996891, 5.629165124598855208, -5.592027715088710771 ) ) ;
#895=VERTEX_POINT ( 'NONE', #9668 ) ;
#949=CARTESIAN_POINT ( 'NONE',  ( -0.5219667817988843384, 7.204195837485507958, -0.5602453477493336553 ) ) ;
#951=MANIFOLD_SOLID_BREP ( 'EndChamfer', #26460 ) ;
#1017=ADVANCED_FACE ( 'NONE', ( #30283 ), #6949, .T. ) ;
#1038=CARTESIAN_POINT ( 'NONE',  ( -1.098735407079250326, -7.248058225758884809, -6.326622577870279152 ) ) ;
#1039=EDGE_LOOP ( 'NONE', ( #23668, #1919 ) ) ;
#1093=CARTESIAN_POINT ( 'NONE',  ( -5.357619327558936585E-16, 7.505553499465137612, -6.064240316920400886 ) ) ;
#1111=CARTESIAN_POINT ( 'NONE',  ( -4.358513833876417998, -4.989164364209884184, -0.07763482564821273801 ) ) ;
#1151=EDGE_LOOP ( 'NONE', ( #25557, #15743, #24197, #1200, #10854, #1528 ) ) ;
#1156=DIRECTION ( 'NONE',  ( -1.000000000000000000, 0.000000000000000000, 0.000000000000000000 ) ) ;
#1174=CARTESIAN_POINT ( 'NONE',  ( -0.5204879950542059541, -7.205049615410630715, -0.5609245978742286587 ) ) ;
#1200=ORIENTED_EDGE ( 'NONE', *, *, #19971, .T. ) ;
#1209=VECTOR ( 'NONE', #26616, 1000.000000000000000 ) ;
#1234=CARTESIAN_POINT ( 'NONE',  ( 6.500000000000000000, -0.6456425506958747285, 7.487771253728014997E-16 ) ) ;
#1240=UNCERTAINTY_MEASURE_WITH_UNIT (LENGTH_MEASURE( 1.000000000000000082E-05 ), #4525, 'distance_accuracy_value', 'NONE');
#1262=CARTESIAN_POINT ( 'NONE',  ( -4.555432764205793461, 5.242992371775927474, -6.208169345099788572 ) ) ;
#1287=CARTESIAN_POINT ( 'NONE',  ( 4.000000000000000000, 0.000000000000000000, -8.000000000000000000 ) ) ;
#1331=CARTESIAN_POINT ( 'NONE',  ( -0.5619217318086660029, -7.564468822943311466, -6.443866470201765395 ) ) ;
#1333=( NAMED_UNIT ( * ) SI_UNIT ( $, .STERADIAN. ) SOLID_ANGLE_UNIT ( ) );
#1366=DIRECTION ( 'NONE',  ( 0.000000000000000000, 0.000000000000000000, 1.000000000000000000 ) ) ;
#1367=CARTESIAN_POINT ( 'NONE',  ( 0.000000000000000000, 0.000000000000000000, -6.800000000000000711 ) ) ;
#1406=EDGE_CURVE ( 'NONE', #29143, #25974, #30427, .T. ) ;
#1443=CARTESIAN_POINT ( 'NONE',  ( -6.815830331203684089, 0.6610623347507950109, -6.171384342982605631 ) ) ;
#1461=CIRCLE ( 'NONE', #24856, 3.399999999999999911 ) ;
#1467=CARTESIAN_POINT ( 'NONE',  ( 6.500000000000000000, 3.752776749732563921, -6.064240316920399110 ) ) ;
#1474=ADVANCED_FACE ( 'NONE', ( #6406 ), #421, .T. ) ;
#1495=DIRECTION ( 'NONE',  ( 0.000000000000000000, 0.000000000000000000, 1.000000000000000000 ) ) ;
#1528=ORIENTED_EDGE ( 'NONE', *, *, #28754, .T. ) ;
#1532=PRODUCT ( 'hex flange nut gradea_iso_ISO - 4161 - M8 - N', 'hex flange nut gradea_iso_ISO - 4161 - M8 - N', '', ( #18240 ) ) ;
#1535=CARTESIAN_POINT ( 'NONE',  ( 2.133938722758552675, 6.273523403446317204, -0.09463688534106567962 ) ) ;
#1585=DIRECTION ( 'NONE',  ( -0.000000000000000000, -0.000000000000000000, 1.000000000000000000 ) ) ;
#1587=CIRCLE ( 'NONE', #5925, 8.331345277524542681 ) ;
#1592=CARTESIAN_POINT ( 'NONE',  ( 6.500000000000000888, 0.000000000000000000, 0.000000000000000000 ) ) ;
#1680=CARTESIAN_POINT ( 'NONE',  ( 6.837824896291514243, -3.947820044545437224, -6.564402953523717166 ) ) ;
#1688=ORIENTED_EDGE ( 'NONE', *, *, #26058, .F. ) ;
#1693=CARTESIAN_POINT ( 'NONE',  ( 6.499999999999999112, -3.752776749732576356, -0.8000000000000003775 ) ) ;
#1726=ORIENTED_EDGE ( 'NONE', *, *, #20401, .F. ) ;
#1779=CARTESIAN_POINT ( 'NONE',  ( 2.075968632158072591, 6.306992450858666110, -6.056431503347234013 ) ) ;
#1812=CARTESIAN_POINT ( 'NONE',  ( -6.500000000000000000, 0.3213925021621126255, 6.556035011748282652E-16 ) ) ;
#1823=ORIENTED_EDGE ( 'NONE', *, *, #23098, .F. ) ;
#1832=STYLED_ITEM ( 'NONE', ( #2148 ), #15696 ) ;
#1875=CARTESIAN_POINT ( 'NONE',  ( 2.688402820137697713, 5.953403407568487182, -0.01956314070068190455 ) ) ;
#1886=DIRECTION ( 'NONE',  ( 1.000000000000000000, 0.000000000000000000, 0.000000000000000000 ) ) ;
#1895=CARTESIAN_POINT ( 'NONE',  ( -1.860983896653666838E-15, 7.693909156113836190, -6.460786012259834621 ) ) ;
#1904=FACE_BOUND ( 'NONE', #21541, .T. ) ;
#1909=ADVANCED_FACE ( 'NONE', ( #26594 ), #24551, .F. ) ;
#1919=ORIENTED_EDGE ( 'NONE', *, *, #8328, .F. ) ;
#1957=FACE_OUTER_BOUND ( 'NONE', #2642, .T. ) ;
#1961=ORIENTED_EDGE ( 'NONE', *, *, #28033, .F. ) ;
#2003=FACE_OUTER_BOUND ( 'NONE', #30107, .T. ) ;
#2012=CARTESIAN_POINT ( 'NONE',  ( 2.075968632162763061, -6.306992450856140131, -6.056431503344847478 ) ) ;
#2048=CARTESIAN_POINT ( 'NONE',  ( 4.555094537983153558, 5.243183837310242623, -6.208110906918258287 ) ) ;
#2081=B_SPLINE_CURVE_WITH_KNOTS ( 'NONE', 3,
 ( #9283, #32286, #6561, #3835, #24964 ),
 .UNSPECIFIED., .F., .F.,
 ( 4, 1, 4 ),
 ( 0.000000000000000000, 0.003752776749732569198, 0.007505553499465138396 ),
 .UNSPECIFIED. ) ;
#2091=CARTESIAN_POINT ( 'NONE',  ( 6.500000000000000000, 3.752776749732573247, -0.8000000000000003775 ) ) ;
#2102=CARTESIAN_POINT ( 'NONE',  ( 3.783380760145018981E-16, -7.895640089090872671, -6.564402953523720718 ) ) ;
#2127=ORIENTED_EDGE ( 'NONE', *, *, #19919, .T. ) ;
#2130=CARTESIAN_POINT ( 'NONE',  ( -6.818286579240217193, 1.325012739682870810, -6.208253321455267759 ) ) ;
#2148=PRESENTATION_STYLE_ASSIGNMENT (( #2312 ) ) ;
#2153=CARTESIAN_POINT ( 'NONE',  ( -6.500000000000000888, 4.076783350660894811, -6.121918786669029444 ) ) ;
#2175=ORIENTED_EDGE ( 'NONE', *, *, #25017, .T. ) ;
#2190=ADVANCED_FACE ( 'NONE', ( #32712 ), #20065, .F. ) ;
#2246=ORIENTED_EDGE ( 'NONE', *, *, #23328, .F. ) ;
#2312=SURFACE_STYLE_USAGE ( .BOTH. , #33150 ) ;
#2346=CARTESIAN_POINT ( 'NONE',  ( 6.818262094730843437, 1.323628772216571381, -6.207787212118422104 ) ) ;
#2387=CARTESIAN_POINT ( 'NONE',  ( -6.815830331203685866, -1.210827632163352847E-13, -6.171384342982610960 ) ) ;
#2404=AXIS2_PLACEMENT_3D ( 'NONE', #8872, #11941, #4266 ) ;
#2410=DIRECTION ( 'NONE',  ( 0.000000000000000000, 0.000000000000000000, 1.000000000000000000 ) ) ;
#2421=AXIS2_PLACEMENT_3D ( 'NONE', #12261, #33039, #11932 ) ;
#2430=EDGE_CURVE ( 'NONE', #17495, #24155, #17726, .T. ) ;
#2513=CARTESIAN_POINT ( 'NONE',  ( 6.815765296784352500, 0.6502800852031724865, -6.170377922158368555 ) ) ;
#2520=CIRCLE ( 'NONE', #5235, 6.500000000000000888 ) ;
#2528=EDGE_CURVE ( 'NONE', #5597, #5932, #1587, .T. ) ;
#2549=CARTESIAN_POINT ( 'NONE',  ( 6.500000000000000000, 3.752776749732563921, -8.000000000000000000 ) ) ;
#2554=ORIENTED_EDGE ( 'NONE', *, *, #28844, .F. ) ;
#2585=CARTESIAN_POINT ( 'NONE',  ( -3.250000000000003997, -5.629165124598849879, 0.000000000000000000 ) ) ;
#2596=TOROIDAL_SURFACE ( 'NONE', #21608, 8.331345277524542681, 0.6186547224754559426 ) ;
#2627=AXIS2_PLACEMENT_3D ( 'NONE', #9466, #21900, #19349 ) ;
#2642=EDGE_LOOP ( 'NONE', ( #28613, #26321, #25959, #14763 ) ) ;
#2649=EDGE_LOOP ( 'NONE', ( #10358, #32918, #23450 ) ) ;
#2897=EDGE_CURVE ( 'NONE', #615, #895, #20173, .T. ) ;
#2977=EDGE_LOOP ( 'NONE', ( #23465, #13032, #17791, #8041 ) ) ;
#3070=LINE ( 'NONE', #13792, #17568 ) ;
#3077=LINE ( 'NONE', #13465, #20258 ) ;
#3084=EDGE_LOOP ( 'NONE', ( #29396, #6006, #4591, #24966, #16927, #3331, #5268 ) ) ;
#3085=CARTESIAN_POINT ( 'NONE',  ( 0.000000000000000000, 0.000000000000000000, -7.974599999999998801 ) ) ;
#3102=TOROIDAL_SURFACE ( 'NONE', #23771, 8.331345277524542681, 0.6186547224754559426 ) ;
#3191=CARTESIAN_POINT ( 'NONE',  ( -1.098735407080685844, 7.248058225761802476, -6.326622577871337860 ) ) ;
#3205=ORIENTED_EDGE ( 'NONE', *, *, #31790, .F. ) ;
#3208=ORIENTED_EDGE ( 'NONE', *, *, #24249, .F. ) ;
#3244=ORIENTED_EDGE ( 'NONE', *, *, #2528, .F. ) ;
#3270=CARTESIAN_POINT ( 'NONE',  ( 6.826425371444817536, -2.641426549045776451, -6.344843397090116355 ) ) ;
#3331=ORIENTED_EDGE ( 'NONE', *, *, #15173, .T. ) ;
#3349=CARTESIAN_POINT ( 'NONE',  ( -2.241046694639089232, 6.576374040525770681, -6.171384342982497273 ) ) ;
#3366=AXIS2_PLACEMENT_3D ( 'NONE', #30771, #20379, #27859 ) ;
#3372=CARTESIAN_POINT ( 'NONE',  ( 0.000000000000000000, 0.000000000000000000, -0.4201245229258211977 ) ) ;
#3393=CARTESIAN_POINT ( 'NONE',  ( -1.049032378834002577, -6.899894373156699068, -0.3607371497494579748 ) ) ;
#3407=EDGE_LOOP ( 'NONE', ( #13104, #13972, #13638, #27288, #10278 ) ) ;
#3474=EDGE_CURVE ( 'NONE', #5597, #4891, #5508, .T. ) ;
#3494=CIRCLE ( 'NONE', #11124, 6.500000000000000888 ) ;
#3505=CARTESIAN_POINT ( 'NONE',  ( 6.838249506730350369, 3.995160516047499222, -6.573190279698081895 ) ) ;
#3515=DIRECTION ( 'NONE',  ( -0.000000000000000000, -0.000000000000000000, 1.000000000000000000 ) ) ;
#3533=ORIENTED_EDGE ( 'NONE', *, *, #31790, .T. ) ;
#3562=CARTESIAN_POINT ( 'NONE',  ( -4.000000000000000000, 4.898587196589412829E-16, -8.000000000000000000 ) ) ;
#3581=EDGE_LOOP ( 'NONE', ( #11425, #8446, #24878, #14814 ) ) ;
#3593=DIRECTION ( 'NONE',  ( 1.000000000000000000, 0.000000000000000000, 0.000000000000000000 ) ) ;
#3657=CARTESIAN_POINT ( 'NONE',  ( -3.809068165403726614, -5.306386968807666804, -4.619717694324952472E-15 ) ) ;
#3681=EDGE_CURVE ( 'NONE', #320, #29326, #29049, .T. ) ;
#3697=LINE ( 'NONE', #14254, #29237 ) ;
#3751=CARTESIAN_POINT ( 'NONE',  ( 4.639619758716984954, -4.826867782832383824, -0.1499059597315342829 ) ) ;
#3756=ORIENTED_EDGE ( 'NONE', *, *, #13315, .T. ) ;
#3779=CARTESIAN_POINT ( 'NONE',  ( -5.416666666666670515, 4.378239541354659536, -5.848636054922036642 ) ) ;
#3835=CARTESIAN_POINT ( 'NONE',  ( -1.083333333333333037, -6.880090707843053544, -5.848636054922041083 ) ) ;
#3866=ORIENTED_EDGE ( 'NONE', *, *, #15173, .F. ) ;
#3915=EDGE_LOOP ( 'NONE', ( #2246, #28577, #22269, #2127, #652 ) ) ;
#4028=B_SPLINE_CURVE_WITH_KNOTS ( 'NONE', 3,
 ( #12052, #1331, #30282, #20226, #27220, #4561, #24832, #14268, #32661, #29949 ),
 .UNSPECIFIED., .F., .F.,
 ( 4, 2, 2, 2, 4 ),
 ( 0.000000000000000000, 0.001989602278884366159, 0.003979204557768732317, 0.005968806836653096741, 0.007958409115537461165 ),
 .UNSPECIFIED. ) ;
#4040=EDGE_LOOP ( 'NONE', ( #33510, #13113, #3533, #11933 ) ) ;
#4094=DIRECTION ( 'NONE',  ( -0.8191520442889917986, 0.000000000000000000, -0.5735764363510460484 ) ) ;
#4109=ADVANCED_FACE ( 'NONE', ( #20834 ), #23485, .T. ) ;
#4111=FACE_OUTER_BOUND ( 'NONE', #1151, .T. ) ;
#4124=CARTESIAN_POINT ( 'NONE',  ( -4.336808689942017736E-16, 7.505553499465137612, -0.8000000000000003775 ) ) ;
#4134=CARTESIAN_POINT ( 'NONE',  ( 0.000000000000000000, 0.000000000000000000, -0.4621369752184044666 ) ) ;
#4167=ORIENTED_EDGE ( 'NONE', *, *, #27629, .T. ) ;
#4184=LINE ( 'NONE', #6578, #11041 ) ;
#4256=CARTESIAN_POINT ( 'NONE',  ( 3.978477517404916064, 5.573260695678954768, -6.171287963165197787 ) ) ;
#4266=DIRECTION ( 'NONE',  ( 1.000000000000000000, 0.000000000000000000, 0.000000000000000000 ) ) ;
#4287=CARTESIAN_POINT ( 'NONE',  ( -12.99999999999999112, -3.903127820947815962E-15, 0.000000000000000000 ) ) ;
#4303=EDGE_CURVE ( 'NONE', #29326, #14989, #20782, .T. ) ;
#4372=DIRECTION ( 'NONE',  ( 0.000000000000000000, 0.000000000000000000, -1.000000000000000000 ) ) ;
#4393=CARTESIAN_POINT ( 'NONE',  ( -0.04050535873993951069, -7.919512791578242172, -6.573129608219095310 ) ) ;
#4454=ORIENTED_EDGE ( 'NONE', *, *, #1406, .F. ) ;
#4461=VECTOR ( 'NONE', #12793, 1000.000000000000000 ) ;
#4481=CARTESIAN_POINT ( 'NONE',  ( 6.500000000000000000, 1.602771114417268050, -0.1495523863686167576 ) ) ;
#4493=ORIENTED_EDGE ( 'NONE', *, *, #25434, .T. ) ;
#4509=CARTESIAN_POINT ( 'NONE',  ( 0.9108756637626340691, 6.979659189792313256, -6.219623095964331050 ) ) ;
#4525=( LENGTH_UNIT ( ) NAMED_UNIT ( * ) SI_UNIT ( .MILLI., .METRE. ) );
#4561=CARTESIAN_POINT ( 'NONE',  ( -3.978477517404915176, -5.573260695678958321, -6.171287963165198676 ) ) ;
#4569=CARTESIAN_POINT ( 'NONE',  ( 0.8808064505790902388, -6.997019658119350005, -5.875704392893848826 ) ) ;
#4591=ORIENTED_EDGE ( 'NONE', *, *, #29161, .T. ) ;
#4598=ORIENTED_EDGE ( 'NONE', *, *, #21604, .F. ) ;
#4631=DIRECTION ( 'NONE',  ( 1.000000000000000000, 0.000000000000000000, -0.000000000000000000 ) ) ;
#4657=CARTESIAN_POINT ( 'NONE',  ( 6.500000000000000000, 3.752776749732573247, -0.8000000000000003775 ) ) ;
#4676=CARTESIAN_POINT ( 'NONE',  ( -6.826425371444817536, 2.641426549045769345, -6.344843397090116355 ) ) ;
#4680=CARTESIAN_POINT ( 'NONE',  ( 5.619193549421086509, 4.261310591078260046, -5.875704392893767114 ) ) ;
#4707=CARTESIAN_POINT ( 'NONE',  ( -6.499999999999999112, 1.286902272306389428, -0.09436334093186068972 ) ) ;
#4732=CARTESIAN_POINT ( 'NONE',  ( 5.727634848075544127, -4.575561887445499742, -6.326622577869666308 ) ) ;
#4764=CARTESIAN_POINT ( 'NONE',  ( 3.250000000000004441, 5.629165124598849879, 0.000000000000000000 ) ) ;
#4773=CARTESIAN_POINT ( 'NONE',  ( -3.999999999999999112, 0.000000000000000000, -7.974599999999998801 ) ) ;
#4777=CARTESIAN_POINT ( 'NONE',  ( -6.826399921716642005, -2.638123634694629516, -6.344399053232583796 ) ) ;
#4798=EDGE_CURVE ( 'NONE', #22066, #29326, #9807, .T. ) ;
#4850=CARTESIAN_POINT ( 'NONE',  ( 4.574783636564339950, 5.228990388887490681, -6.171384342982508819 ) ) ;
#4891=VERTEX_POINT ( 'NONE', #12964 ) ;
#4938=EDGE_CURVE ( 'NONE', #5394, #24155, #20962, .T. ) ;
#4946=CARTESIAN_POINT ( 'NONE',  ( 0.000000000000000000, 0.000000000000000000, -8.000000000000000000 ) ) ;
#4999=DIRECTION ( 'NONE',  ( 0.000000000000000000, 0.000000000000000000, -1.000000000000000000 ) ) ;
#5020=CARTESIAN_POINT ( 'NONE',  ( -0.04050535873993896946, 7.919512791578231514, -6.573129608219091757 ) ) ;
#5056=ORIENTED_EDGE ( 'NONE', *, *, #2430, .T. ) ;
#5070=EDGE_LOOP ( 'NONE', ( #26447, #15986, #25757, #5642 ) ) ;
#5101=MECHANICAL_DESIGN_GEOMETRIC_PRESENTATION_REPRESENTATION('',(#1832),#29026);
#5104=CARTESIAN_POINT ( 'NONE',  ( 6.831979103402612274, 3.295157223185832596, -6.443785395948806283 ) ) ;
#5128=FACE_OUTER_BOUND ( 'NONE', #6845, .T. ) ;
#5185=DIRECTION ( 'NONE',  ( 0.8660254037844382635, -0.5000000000000006661, 0.000000000000000000 ) ) ;
#5186=ORIENTED_EDGE ( 'NONE', *, *, #20771, .F. ) ;
#5194=CARTESIAN_POINT ( 'NONE',  ( 0.000000000000000000, 0.000000000000000000, 0.000000000000000000 ) ) ;
#5235=AXIS2_PLACEMENT_3D ( 'NONE', #23111, #12546, #22937 ) ;
#5266=CARTESIAN_POINT ( 'NONE',  ( 6.837824896291514243, 3.947820044545427454, -6.564402953523716278 ) ) ;
#5267=CARTESIAN_POINT ( 'NONE',  ( 0.000000000000000000, 0.000000000000000000, -7.974599999999998801 ) ) ;
#5268=ORIENTED_EDGE ( 'NONE', *, *, #20104, .T. ) ;
#5294=CARTESIAN_POINT ( 'NONE',  ( 0.000000000000000000, 0.000000000000000000, -7.974599999999998801 ) ) ;
#5310=STYLED_ITEM ( 'NONE', ( #16991 ), #951 ) ;
#5394=VERTEX_POINT ( 'NONE', #3562 ) ;
#5446=ORIENTED_EDGE ( 'NONE', *, *, #20018, .F. ) ;
#5469=EDGE_LOOP ( 'NONE', ( #10219, #15728, #33186, #21722, #19459 ) ) ;
#5508=CIRCLE ( 'NONE', #15841, 0.6186547224754559426 ) ;
#5519=ORIENTED_EDGE ( 'NONE', *, *, #381, .T. ) ;
#5552=UNCERTAINTY_MEASURE_WITH_UNIT (LENGTH_MEASURE( 1.000000000000000082E-05 ), #29579, 'distance_accuracy_value', 'NONE');
#5570=CARTESIAN_POINT ( 'NONE',  ( 6.500000000000000000, 3.752776749732563921, -6.064240316920399110 ) ) ;
#5572=ADVANCED_FACE ( 'NONE', ( #25812 ), #30927, .T. ) ;
#5577=CARTESIAN_POINT ( 'NONE',  ( -5.589124336234651658, 4.278671059406048194, -6.219623095967983240 ) ) ;
#5597=VERTEX_POINT ( 'NONE', #31097 ) ;
#5642=ORIENTED_EDGE ( 'NONE', *, *, #31264, .F. ) ;
#5735=CARTESIAN_POINT ( 'NONE',  ( -5.357619327558936585E-16, 7.505553499465137612, -8.000000000000000000 ) ) ;
#5736=CARTESIAN_POINT ( 'NONE',  ( 6.500000000000000000, -3.752776749732574135, -6.064240316920400886 ) ) ;
#5764=DIRECTION ( 'NONE',  ( 1.000000000000000000, 0.000000000000000000, 0.000000000000000000 ) ) ;
#5785=ORIENTED_EDGE ( 'NONE', *, *, #3474, .F. ) ;
#5826=VERTEX_POINT ( 'NONE', #21025 ) ;
#5925=AXIS2_PLACEMENT_3D ( 'NONE', #4946, #26393, #15334 ) ;
#5932=VERTEX_POINT ( 'NONE', #13355 ) ;
#5967=CARTESIAN_POINT ( 'NONE',  ( 0.2259792476677697226, -7.636022678937403718, -6.470294263593365791 ) ) ;
#6006=ORIENTED_EDGE ( 'NONE', *, *, #28033, .T. ) ;
#6053=CARTESIAN_POINT ( 'NONE',  ( -1.058054217398698871, 6.894685612232779981, -0.3576316571898437990 ) ) ;
#6058=CYLINDRICAL_SURFACE ( 'NONE', #19763, 3.399999999999999911 ) ;
#6126=EDGE_LOOP ( 'NONE', ( #14367, #2554, #28780 ) ) ;
#6128=EDGE_LOOP ( 'NONE', ( #40, #27379, #2175, #1726 ) ) ;
#6219=ORIENTED_EDGE ( 'NONE', *, *, #29106, .F. ) ;
#6241=CARTESIAN_POINT ( 'NONE',  ( -6.725979247667768668, 3.622307570260310694, -6.470294263593358686 ) ) ;
#6282=DIRECTION ( 'NONE',  ( 0.000000000000000000, 0.000000000000000000, 1.000000000000000000 ) ) ;
#6285=DIRECTION ( 'NONE',  ( -0.8191520442889923537, 1.003171929053525363E-16, 0.5735764363510453823 ) ) ;
#6295=CARTESIAN_POINT ( 'NONE',  ( 5.450967621166010524, -4.358435876041012236, -0.3607371497494579193 ) ) ;
#6301=CARTESIAN_POINT ( 'NONE',  ( -2.055025722541619970, -6.319083845364135144, -5.720331885005373707 ) ) ;
#6334=B_SPLINE_CURVE_WITH_KNOTS ( 'NONE', 3,
 ( #29037, #32089, #11150, #8752, #26803 ),
 .UNSPECIFIED., .F., .F.,
 ( 4, 1, 4 ),
 ( 0.000000000000000000, 0.003752776749732568765, 0.007505553499465137529 ),
 .UNSPECIFIED. ) ;
#6370=( GEOMETRIC_REPRESENTATION_CONTEXT ( 3 ) GLOBAL_UNCERTAINTY_ASSIGNED_CONTEXT ( ( #26674 ) ) GLOBAL_UNIT_ASSIGNED_CONTEXT ( ( #27550, #14270, #1333 ) ) REPRESENTATION_CONTEXT ( 'NONE', 'WORKASPACE' ) );
#6379=VECTOR ( 'NONE', #10462, 1000.000000000000000 ) ;
#6392=ORIENTED_EDGE ( 'NONE', *, *, #9785, .F. ) ;
#6395=AXIS2_PLACEMENT_3D ( 'NONE', #20064, #14274, #21943 ) ;
#6400=DIRECTION ( 'NONE',  ( -1.000000000000000000, 0.000000000000000000, 0.000000000000000000 ) ) ;
#6402=EDGE_CURVE ( 'NONE', #20607, #14989, #13873, .T. ) ;
#6406=FACE_OUTER_BOUND ( 'NONE', #19328, .T. ) ;
#6477=B_SPLINE_CURVE_WITH_KNOTS ( 'NONE', 3,
 ( #11007, #8612, #14400, #27177, #17123, #14055 ),
 .UNSPECIFIED., .F., .F.,
 ( 4, 2, 4 ),
 ( 0.003841072314098346787, 0.005765657563962181195, 0.007690242813826015170 ),
 .UNSPECIFIED. ) ;
#6479=EDGE_CURVE ( 'NONE', #29326, #19336, #13910, .T. ) ;
#6513=CARTESIAN_POINT ( 'NONE',  ( -6.539196172009840602, -3.775406670193658165, -6.286444963328103874 ) ) ;
#6539=CARTESIAN_POINT ( 'NONE',  ( 1.083333333333333703, 6.880090707843044662, -5.848636054922036642 ) ) ;
#6555=CARTESIAN_POINT ( 'NONE',  ( -3.399999999999999911, 4.163799117101000559E-16, -7.554475477074173106 ) ) ;
#6561=CARTESIAN_POINT ( 'NONE',  ( -3.250000000000000444, -5.629165124598859649, -5.592027715088708995 ) ) ;
#6570=DIRECTION ( 'NONE',  ( -0.000000000000000000, -0.000000000000000000, 1.000000000000000000 ) ) ;
#6578=CARTESIAN_POINT ( 'NONE',  ( -8.542937654374687995, 0.000000000000000000, -6.800000000000000711 ) ) ;
#6646=CARTESIAN_POINT ( 'NONE',  ( 3.399999999999999911, 0.000000000000000000, -8.000000000000000000 ) ) ;
#6680=VERTEX_POINT ( 'NONE', #12366 ) ;
#6693=CARTESIAN_POINT ( 'NONE',  ( 5.978033218201114884, 4.054134411712192687, -0.5602453477493293255 ) ) ;
#6748=CARTESIAN_POINT ( 'NONE',  ( -6.500000000000000000, -3.155218591052673549, -0.5622968210053901350 ) ) ;
#6757=AXIS2_PLACEMENT_3D ( 'NONE', #9161, #19556, #27887 ) ;
#6779=DIRECTION ( 'NONE',  ( 0.8660254037844382635, 0.5000000000000004441, 0.000000000000000000 ) ) ;
#6783=CARTESIAN_POINT ( 'NONE',  ( -0.2813450144774474748, -7.667988119308860817, -6.122077150241856280 ) ) ;
#6838=DIRECTION ( 'NONE',  ( -0.5000000000000006661, 0.8660254037844382635, 0.000000000000000000 ) ) ;
#6845=EDGE_LOOP ( 'NONE', ( #3244, #4598 ) ) ;
#6872=CARTESIAN_POINT ( 'NONE',  ( 6.500000000000000000, 0.6470732608156823940, -0.01945970098673075951 ) ) ;
#6939=AXIS2_PLACEMENT_3D ( 'NONE', #14707, #27158, #24772 ) ;
#6949=PLANE ( 'NONE',  #25418 ) ;
#6952=CARTESIAN_POINT ( 'NONE',  ( 0.000000000000000000, 0.000000000000000000, 0.000000000000000000 ) ) ;
#6979=ORIENTED_EDGE ( 'NONE', *, *, #27629, .F. ) ;
#6998=ORIENTED_EDGE ( 'NONE', *, *, #25390, .T. ) ;
#7091=CARTESIAN_POINT ( 'NONE',  ( 6.663127973346137267, 3.846958729056316528, -6.460793508093409798 ) ) ;
#7099=ADVANCED_FACE ( 'NONE', ( #13206 ), #28372, .F. ) ;
#7156=CARTESIAN_POINT ( 'NONE',  ( 0.5204879950541921874, 7.205049615410631603, -0.5609245978742269934 ) ) ;
#7177=DIRECTION ( 'NONE',  ( -1.000000000000000000, 0.000000000000000000, 0.000000000000000000 ) ) ;
#7180=CARTESIAN_POINT ( 'NONE',  ( -5.357619327558936585E-16, 7.505553499465137612, -8.000000000000000000 ) ) ;
#7213=CARTESIAN_POINT ( 'NONE',  ( 6.500000000000000000, 2.227636940139130051, -0.2900584647821234374 ) ) ;
#7232=EDGE_LOOP ( 'NONE', ( #27845, #29053, #26774, #6979 ) ) ;
#7241=FACE_OUTER_BOUND ( 'NONE', #24373, .T. ) ;
#7247=DIRECTION ( 'NONE',  ( 0.000000000000000000, 0.000000000000000000, -1.000000000000000000 ) ) ;
#7263=CARTESIAN_POINT ( 'NONE',  ( -6.500000000000000000, -0.6456425506958733962, 7.521652571618187011E-16 ) ) ;
#7310=CARTESIAN_POINT ( 'NONE',  ( 8.331345277524542681, 0.000000000000000000, -7.381345277524544279 ) ) ;
#7314=DIRECTION ( 'NONE',  ( 1.000000000000000000, 0.000000000000000000, 0.000000000000000000 ) ) ;
#7428=AXIS2_PLACEMENT_3D ( 'NONE', #17236, #22015, #9063 ) ;
#7455=ORIENTED_EDGE ( 'NONE', *, *, #12870, .T. ) ;
#7543=AXIS2_PLACEMENT_3D ( 'NONE', #9665, #1156, #1495 ) ;
#7573=AXIS2_PLACEMENT_3D ( 'NONE', #4287, #9912, #4631 ) ;
#7639=CARTESIAN_POINT ( 'NONE',  ( 0.000000000000000000, 0.000000000000000000, -7.381345277524544279 ) ) ;
#7648=CARTESIAN_POINT ( 'NONE',  ( -6.500000000000005329, 3.752776749732560813, -6.177802698399430525 ) ) ;
#7701=ORIENTED_EDGE ( 'NONE', *, *, #25197, .T. ) ;
#7757=VERTEX_POINT ( 'NONE', #28847 ) ;
#7817=CARTESIAN_POINT ( 'NONE',  ( 5.698650001973517121, -4.592339236403569558, -6.344532336093708480 ) ) ;
#7818=AXIS2_PLACEMENT_3D ( 'NONE', #15570, #15903, #5185 ) ;
#7842=CIRCLE ( 'NONE', #749, 3.999999999999999112 ) ;
#8041=ORIENTED_EDGE ( 'NONE', *, *, #2430, .F. ) ;
#8123=CARTESIAN_POINT ( 'NONE',  ( -6.500000000000000000, 3.752776749732564809, -8.000000000000000000 ) ) ;
#8152=CARTESIAN_POINT ( 'NONE',  ( 6.500000000000002665, 2.501851166488374911, -5.848636054922036642 ) ) ;
#8172=DIRECTION ( 'NONE',  ( 0.000000000000000000, 0.000000000000000000, -1.000000000000000000 ) ) ;
#8244=B_SPLINE_CURVE_WITH_KNOTS ( 'NONE', 3,
 ( #12445, #9376, #22835, #32883, #20274 ),
 .UNSPECIFIED., .F., .F.,
 ( 4, 1, 4 ),
 ( 5.644705275899819452E-20, 0.003752776749732567464, 0.007505553499465136662 ),
 .UNSPECIFIED. ) ;
#8248=ORIENTED_EDGE ( 'NONE', *, *, #16047, .F. ) ;
#8324=VERTEX_POINT ( 'NONE', #2585 ) ;
#8328=EDGE_CURVE ( 'NONE', #5394, #24271, #13567, .T. ) ;
#8379=CARTESIAN_POINT ( 'NONE',  ( 6.500000000000000000, 3.752776749732563921, -6.064240316920399110 ) ) ;
#8395=CARTESIAN_POINT ( 'NONE',  ( 6.831985876597697072, -3.295913427296349951, -6.443925148804115821 ) ) ;
#8396=CIRCLE ( 'NONE', #31777, 6.500000000000000888 ) ;
#8429=ORIENTED_EDGE ( 'NONE', *, *, #28844, .T. ) ;
#8446=ORIENTED_EDGE ( 'NONE', *, *, #8328, .T. ) ;
#8467=CARTESIAN_POINT ( 'NONE',  ( -0.8808064505788995024, 6.997019658119450369, -5.875704392893736916 ) ) ;
#8507=CARTESIAN_POINT ( 'NONE',  ( -2.688402820137703930, -5.953403407568491623, -0.01956314070068837160 ) ) ;
#8526=VERTEX_POINT ( 'NONE', #10752 ) ;
#8528=CARTESIAN_POINT ( 'NONE',  ( -0.8808064505793390397, -6.997019658119205232, -5.875704392894199657 ) ) ;
#8531=DIRECTION ( 'NONE',  ( -1.000000000000000000, 0.000000000000000000, 0.000000000000000000 ) ) ;
#8595=CARTESIAN_POINT ( 'NONE',  ( -6.826296012759691223, -2.664253980652245168, -6.325071479460635970 ) ) ;
#8612=CARTESIAN_POINT ( 'NONE',  ( 2.690931834596283156, -5.951943280390046276, -5.793705359219412742E-15 ) ) ;
#8620=CARTESIAN_POINT ( 'NONE',  ( -3.250000000000004441, 5.629165124598849879, 0.000000000000000000 ) ) ;
#8658=DIRECTION ( 'NONE',  ( 1.000000000000000000, 0.000000000000000000, 0.000000000000000000 ) ) ;
#8747=ORIENTED_EDGE ( 'NONE', *, *, #6479, .F. ) ;
#8752=CARTESIAN_POINT ( 'NONE',  ( -6.500000000000002665, -2.501851166488385125, -5.848636054922036642 ) ) ;
#8756=CARTESIAN_POINT ( 'NONE',  ( -6.500000000000000888, 0.000000000000000000, 0.000000000000000000 ) ) ;
#8760=CARTESIAN_POINT ( 'NONE',  ( -6.815962252199548210, 1.383413844627830791, -6.173425845474762141 ) ) ;
#8796=CARTESIAN_POINT ( 'NONE',  ( 0.2813450144774485850, 7.667988119308852824, -6.122077150241853616 ) ) ;
#8815=LINE ( 'NONE', #495, #31995 ) ;
#8872=CARTESIAN_POINT ( 'NONE',  ( 0.000000000000000000, 0.000000000000000000, 0.000000000000000000 ) ) ;
#8899=CARTESIAN_POINT ( 'NONE',  ( 6.500000000000000000, -3.155218591052677990, -0.5622968210053915783 ) ) ;
#8902=ORIENTED_EDGE ( 'NONE', *, *, #21604, .T. ) ;
#8903=( BOUNDED_SURFACE ( )  B_SPLINE_SURFACE ( 3, 2, ( 
 ( #13637, #696, #24372 ),
 ( #11100, #19260, #21480 ),
 ( #26925, #32367, #27097 ),
 ( #6301, #11590, #32037 ),
 ( #8528, #9031, #1038 ),
 ( #18923, #5967, #16355 ) ),
 .UNSPECIFIED., .F., .F., .T. ) 
 B_SPLINE_SURFACE_WITH_KNOTS ( ( 4, 2, 4 ),
 ( 3, 3 ),
 ( 0.003190620565844225990, 0.007281897438794491043, 0.01137317431174475653 ),
 ( 0.000000000000000000, 1.000000000000000000 ),
 .UNSPECIFIED. ) 
 GEOMETRIC_REPRESENTATION_ITEM ( )  RATIONAL_B_SPLINE_SURFACE ( (
 ( 1.000000000000000000, 0.8047731410850402778, 1.000000000000000000),
 ( 1.000000000000000000, 0.8125552299156234559, 1.000000000000000000),
 ( 1.000000000000000000, 0.8191520442889865805, 1.000000000000000000),
 ( 1.000000000000000000, 0.8191520442889865805, 1.000000000000000000),
 ( 1.000000000000000000, 0.8125552299156227898, 1.000000000000000000),
 ( 1.000000000000000000, 0.8047731410850399447, 1.000000000000000000) ) ) 
 REPRESENTATION_ITEM ( '' )  SURFACE ( )  );
#8905=CIRCLE ( 'NONE', #21964, 3.399999999999999911 ) ;
#8955=FACE_OUTER_BOUND ( 'NONE', #26055, .T. ) ;
#9031=CARTESIAN_POINT ( 'NONE',  ( -0.9108756637647318355, -6.979659189790606177, -6.219623095965800097 ) ) ;
#9063=DIRECTION ( 'NONE',  ( 1.000000000000000000, 0.000000000000000000, 0.000000000000000000 ) ) ;
#9127=AXIS2_PLACEMENT_3D ( 'NONE', #21290, #6282, #13617 ) ;
#9161=CARTESIAN_POINT ( 'NONE',  ( 0.000000000000000000, 0.000000000000000000, -6.800000000000000711 ) ) ;
#9227=CARTESIAN_POINT ( 'NONE',  ( 8.451593625408400647E-13, 7.790254909845287123, -6.526045885145519421 ) ) ;
#9283=CARTESIAN_POINT ( 'NONE',  ( -6.500000000000000000, -3.752776749732572803, -6.064240316920399998 ) ) ;
#9288=CARTESIAN_POINT ( 'NONE',  ( 0.000000000000000000, 0.000000000000000000, -7.381345277524544279 ) ) ;
#9328=FILL_AREA_STYLE_COLOUR ( '', #19995 ) ;
#9368=DIRECTION ( 'NONE',  ( 0.000000000000000000, 0.000000000000000000, 1.000000000000000000 ) ) ;
#9376=CARTESIAN_POINT ( 'NONE',  ( 1.083333333333332593, -6.880090707843051767, -5.848636054922041083 ) ) ;
#9397=PLANE ( 'NONE',  #7573 ) ;
#9412=CARTESIAN_POINT ( 'NONE',  ( 5.441945782601302462, 4.363644636964922441, -0.3576316571898402463 ) ) ;
#9421=CARTESIAN_POINT ( 'NONE',  ( -3.755786496842903988E-16, -7.505553499465146494, -6.064240316920404439 ) ) ;
#9466=CARTESIAN_POINT ( 'NONE',  ( 0.000000000000000000, 0.000000000000000000, 0.000000000000000000 ) ) ;
#9503=CARTESIAN_POINT ( 'NONE',  ( 4.444974277458119793, -4.939246403833736032, -5.720331885005374595 ) ) ;
#9513=CARTESIAN_POINT ( 'NONE',  ( -3.528928113779633335, 5.468125903023623557, 1.037615360386517718E-15 ) ) ;
#9516=CARTESIAN_POINT ( 'NONE',  ( 6.500000000000005329, -3.752776749732570583, -6.177805531628536961 ) ) ;
#9608=EDGE_LOOP ( 'NONE', ( #8747, #21027, #18765, #7455, #18355 ) ) ;
#9647=DIRECTION ( 'NONE',  ( 0.9396926207859143121, 1.150791560227857665E-16, -0.3420201433256525592 ) ) ;
#9654=B_SPLINE_CURVE_WITH_KNOTS ( 'NONE', 3,
 ( #28429, #13090, #7817, #28598, #15480, #31150, #26198, #146, #12757, #18207 ),
 .UNSPECIFIED., .F., .F.,
 ( 4, 2, 2, 2, 4 ),
 ( 0.000000000000000000, 0.001989602278884365291, 0.003979204557768730582, 0.005968806836653095874, 0.007958409115537461165 ),
 .UNSPECIFIED. ) ;
#9665=CARTESIAN_POINT ( 'NONE',  ( 6.500000000000000000, 3.752776749732563921, -8.000000000000000000 ) ) ;
#9668=CARTESIAN_POINT ( 'NONE',  ( 3.999999999999999112, 0.000000000000000000, 3.469446951953614189E-15 ) ) ;
#9743=ORIENTED_EDGE ( 'NONE', *, *, #21984, .T. ) ;
#9748=CARTESIAN_POINT ( 'NONE',  ( 3.399999999999999911, 0.000000000000000000, -7.554475477074173106 ) ) ;
#9781=ORIENTED_EDGE ( 'NONE', *, *, #14945, .F. ) ;
#9785=EDGE_CURVE ( 'NONE', #73, #29143, #8244, .T. ) ;
#9807=B_SPLINE_CURVE_WITH_KNOTS ( 'NONE', 3,
 ( #25232, #9227, #1895, #12282, #22674, #20119 ),
 .UNSPECIFIED., .F., .F.,
 ( 4, 2, 4 ),
 ( -4.604908129291797664E-06, 0.0003318387708545240283, 0.0006682824498383398322 ),
 .UNSPECIFIED. ) ;
#9819=FACE_OUTER_BOUND ( 'NONE', #2649, .T. ) ;
#9830=CARTESIAN_POINT ( 'NONE',  ( -6.500000000000000000, 3.149025070564754003, -0.5705737632551073357 ) ) ;
#9894=CARTESIAN_POINT ( 'NONE',  ( 0.000000000000000000, 0.000000000000000000, -0.4621369752184044666 ) ) ;
#9912=DIRECTION ( 'NONE',  ( 0.000000000000000000, 0.000000000000000000, 1.000000000000000000 ) ) ;
#10032=CARTESIAN_POINT ( 'NONE',  ( 0.9108756637647450471, -6.979659189788935514, -6.219623095965384429 ) ) ;
#10187=CARTESIAN_POINT ( 'NONE',  ( 6.500000000000296652, 3.350125858420170299, -6.343571411523281967 ) ) ;
#10219=ORIENTED_EDGE ( 'NONE', *, *, #29945, .T. ) ;
#10227=VERTEX_POINT ( 'NONE', #31512 ) ;
#10238=B_SPLINE_CURVE_WITH_KNOTS ( 'NONE', 3,
 ( #33166, #1812, #15096, #4707, #30611, #28393, #17321, #9830, #27869, #12208 ),
 .UNSPECIFIED., .F., .F.,
 ( 4, 2, 2, 2, 4 ),
 ( 0.009353627468483380336, 0.01031000219096067302, 0.01126637691343796571, 0.01222275163591525840, 0.01317912635839255109 ),
 .UNSPECIFIED. ) ;
#10253=SHAPE_DEFINITION_REPRESENTATION ( #28218, #17198 ) ;
#10278=ORIENTED_EDGE ( 'NONE', *, *, #18328, .T. ) ;
#10358=ORIENTED_EDGE ( 'NONE', *, *, #13073, .F. ) ;
#10361=CARTESIAN_POINT ( 'NONE',  ( 6.826581433398040133, -2.695947255479557381, -6.331032031596317999 ) ) ;
#10420=CARTESIAN_POINT ( 'NONE',  ( -4.000000000000000000, 4.898587196589412829E-16, -25.03750572909317285 ) ) ;
#10424=ADVANCED_FACE ( 'NONE', ( #14955 ), #11555, .T. ) ;
#10456=ADVANCED_FACE ( 'NONE', ( #25012 ), #20554, .T. ) ;
#10462=DIRECTION ( 'NONE',  ( 0.000000000000000000, 0.000000000000000000, 1.000000000000000000 ) ) ;
#10536=LINE ( 'NONE', #31632, #28101 ) ;
#10539=DIRECTION ( 'NONE',  ( 0.000000000000000000, -1.000000000000000000, 0.000000000000000000 ) ) ;
#10543=CARTESIAN_POINT ( 'NONE',  ( -6.837824896291514243, 3.947820044545427454, -6.564402953523716278 ) ) ;
#10654=ADVANCED_FACE ( 'NONE', ( #20577 ), #2596, .T. ) ;
#10683=CARTESIAN_POINT ( 'NONE',  ( 6.499999999999999112, 4.014041399406598210, -6.470356572124273953 ) ) ;
#10699=VECTOR ( 'NONE', #32500, 1000.000000000000000 ) ;
#10752=CARTESIAN_POINT ( 'NONE',  ( -6.837824896291515131, -3.947820044545435447, -6.564402953523717166 ) ) ;
#10767=VECTOR ( 'NONE', #19523, 1000.000000000000000 ) ;
#10854=ORIENTED_EDGE ( 'NONE', *, *, #20018, .T. ) ;
#10877=ADVANCED_FACE ( 'NONE', ( #26510 ), #6058, .F. ) ;
#10892=DIRECTION ( 'NONE',  ( 0.000000000000000000, 0.000000000000000000, 1.000000000000000000 ) ) ;
#10933=ORIENTED_EDGE ( 'NONE', *, *, #20771, .T. ) ;
#10978=DIRECTION ( 'NONE',  ( -1.000000000000000000, 0.000000000000000000, 0.000000000000000000 ) ) ;
#10989=CONICAL_SURFACE ( 'NONE', #3366, 6.500000000000000888, 0.8987552595851582282 ) ;
#11007=CARTESIAN_POINT ( 'NONE',  ( 3.250000000000003109, -5.629165124598849879, 0.000000000000000000 ) ) ;
#11028=PRODUCT_DEFINITION_FORMATION_WITH_SPECIFIED_SOURCE ( 'ANY', '', #1532, .NOT_KNOWN. ) ;
#11032=CARTESIAN_POINT ( 'NONE',  ( -6.878751942472531411, 3.924677726130923361, -6.573129608219089981 ) ) ;
#11041=VECTOR ( 'NONE', #32802, 1000.000000000000000 ) ;
#11100=CARTESIAN_POINT ( 'NONE',  ( -5.619193549420757883, -4.261310591078458110, -5.875704392893551287 ) ) ;
#11124=AXIS2_PLACEMENT_3D ( 'NONE', #13599, #31664, #8658 ) ;
#11150=CARTESIAN_POINT ( 'NONE',  ( -6.500000000000001776, -2.602085213965210642E-15, -5.592027715088707218 ) ) ;
#11152=EDGE_CURVE ( 'NONE', #5826, #13463, #24285, .T. ) ;
#11159=CARTESIAN_POINT ( 'NONE',  ( -6.500000000000000888, -1.360915494584213459, -5.718331000733963165 ) ) ;
#11282=CARTESIAN_POINT ( 'NONE',  ( 6.818286579240217193, -1.325012739682874141, -6.208253321455268647 ) ) ;
#11425=ORIENTED_EDGE ( 'NONE', *, *, #4938, .F. ) ;
#11555=PLANE ( 'NONE',  #6395 ) ;
#11558=LINE ( 'NONE', #22113, #10699 ) ;
#11571=CARTESIAN_POINT ( 'NONE',  ( -3.250000000000003997, -5.629165124598849879, 0.000000000000000000 ) ) ;
#11589=LINE ( 'NONE', #6646, #448 ) ;
#11590=CARTESIAN_POINT ( 'NONE',  ( -2.075968632161005800, -6.306992450858350807, -6.056431503346042078 ) ) ;
#11632=B_SPLINE_CURVE_WITH_KNOTS ( 'NONE', 3,
 ( #1467, #20031, #30431, #7091, #14580, #22761 ),
 .UNSPECIFIED., .F., .F.,
 ( 4, 2, 4 ),
 ( 0.000000000000000000, 0.0003352299596252128282, 0.0006704599192504256564 ),
 .UNSPECIFIED. ) ;
#11657=CARTESIAN_POINT ( 'NONE',  ( -2.837346585668847787, 6.232092946297378866, -6.171287963165196899 ) ) ;
#11669=ORIENTED_EDGE ( 'NONE', *, *, #2897, .F. ) ;
#11692=( NAMED_UNIT ( * ) SI_UNIT ( $, .STERADIAN. ) SOLID_ANGLE_UNIT ( ) );
#11718=PLANE ( 'NONE',  #7543 ) ;
#11751=B_SPLINE_CURVE_WITH_KNOTS ( 'NONE', 3,
 ( #23035, #25592, #33432, #9412, #6693, #2091 ),
 .UNSPECIFIED., .F., .F.,
 ( 4, 2, 4 ),
 ( 0.003841072314098362400, 0.005765657563962184665, 0.007690242813826007363 ),
 .UNSPECIFIED. ) ;
#11754=EDGE_CURVE ( 'NONE', #8526, #20186, #25135, .T. ) ;
#11756=DIRECTION ( 'NONE',  ( -0.000000000000000000, -0.000000000000000000, 1.000000000000000000 ) ) ;
#11780=B_SPLINE_CURVE_WITH_KNOTS ( 'NONE', 3,
 ( #1693, #22310, #6295, #3751, #25040, #16689, #29817, #17196 ),
 .UNSPECIFIED., .F., .F.,
 ( 4, 2, 2, 4 ),
 ( 2.459764730742321679E-07, 0.001920659145285711104, 0.002880865729692028403, 0.003841072314098346787 ),
 .UNSPECIFIED. ) ;
#11840=CARTESIAN_POINT ( 'NONE',  ( -3.755786496842903988E-16, -7.505553499465146494, -6.064240316920404439 ) ) ;
#11846=AXIS2_PLACEMENT_3D ( 'NONE', #6952, #14778, #22446 ) ;
#11862=CARTESIAN_POINT ( 'NONE',  ( -6.500000000000000000, 3.752776749732564809, -6.064240316920399110 ) ) ;
#11932=DIRECTION ( 'NONE',  ( 1.000000000000000000, 0.000000000000000000, 0.000000000000000000 ) ) ;
#11933=ORIENTED_EDGE ( 'NONE', *, *, #14726, .T. ) ;
#11941=DIRECTION ( 'NONE',  ( 0.000000000000000000, 0.000000000000000000, 1.000000000000000000 ) ) ;
#12052=CARTESIAN_POINT ( 'NONE',  ( 3.783380760145018981E-16, -7.895640089090872671, -6.564402953523720718 ) ) ;
#12054=SURFACE_STYLE_FILL_AREA ( #20061 ) ;
#12059=CARTESIAN_POINT ( 'NONE',  ( 6.725979247667765115, -3.622307570260320020, -6.470294263593358686 ) ) ;
#12098=EDGE_CURVE ( 'NONE', #73, #23539, #16569, .T. ) ;
#12158=CARTESIAN_POINT ( 'NONE',  ( -1.269541193505925744E-15, 7.895640089090863789, -6.564402953523717166 ) ) ;
#12179=CARTESIAN_POINT ( 'NONE',  ( 6.725979247667768668, 3.622307570260308918, -6.470294263593358686 ) ) ;
#12208=CARTESIAN_POINT ( 'NONE',  ( -6.500000000000000000, 3.752776749732564809, -0.7999999999999969358 ) ) ;
#12219=ORIENTED_EDGE ( 'NONE', *, *, #19981, .T. ) ;
#12225=CARTESIAN_POINT ( 'NONE',  ( -3.250000000000004441, 5.629165124598849879, 0.000000000000000000 ) ) ;
#12261=CARTESIAN_POINT ( 'NONE',  ( 0.000000000000000000, 0.000000000000000000, 0.000000000000000000 ) ) ;
#12282=CARTESIAN_POINT ( 'NONE',  ( -1.013799215429234768E-15, 7.550813340387307449, -6.286444963328104762 ) ) ;
#12304=ORIENTED_EDGE ( 'NONE', *, *, #13315, .F. ) ;
#12365=CARTESIAN_POINT ( 'NONE',  ( -6.499999999999999112, -1.280811194704858158, -0.07768058122908438889 ) ) ;
#12366=CARTESIAN_POINT ( 'NONE',  ( 3.250000000000003109, -5.629165124598849879, 0.000000000000000000 ) ) ;
#12394=CARTESIAN_POINT ( 'NONE',  ( 6.500000000000576428, -2.723981882618385697, -6.224051986860747121 ) ) ;
#12400=CARTESIAN_POINT ( 'NONE',  ( 2.055025722541879318, -6.319083845363985930, -5.720331885005374595 ) ) ;
#12436=CARTESIAN_POINT ( 'NONE',  ( 5.699988423468465015, 4.591578518468247161, -6.344710093416081165 ) ) ;
#12445=CARTESIAN_POINT ( 'NONE',  ( -3.755786496842903988E-16, -7.505553499465146494, -6.064240316920404439 ) ) ;
#12460=ADVANCED_FACE ( 'NONE', ( #27279 ), #13804, .T. ) ;
#12520=CARTESIAN_POINT ( 'NONE',  ( 4.424031367836657402, 4.951337798342080099, -6.056431503344841261 ) ) ;
#12521=ORIENTED_EDGE ( 'NONE', *, *, #22078, .T. ) ;
#12546=DIRECTION ( 'NONE',  ( 0.000000000000000000, 0.000000000000000000, 1.000000000000000000 ) ) ;
#12596=B_SPLINE_CURVE_WITH_KNOTS ( 'NONE', 3,
 ( #25287, #1443, #2130, #4676, #20175, #30573 ),
 .UNSPECIFIED., .F., .F.,
 ( 4, 2, 4 ),
 ( 0.003981881017442828914, 0.005970145066490142871, 0.007958409115537457695 ),
 .UNSPECIFIED. ) ;
#12628=ORIENTED_EDGE ( 'NONE', *, *, #23328, .T. ) ;
#12736=CARTESIAN_POINT ( 'NONE',  ( 6.500000000000000888, 3.402385889607308922, -5.998095356498452269 ) ) ;
#12747=AXIS2_PLACEMENT_3D ( 'NONE', #1367, #11756, #22315 ) ;
#12757=CARTESIAN_POINT ( 'NONE',  ( 0.5620262070071402327, -7.564407249984300918, -6.443844059477449093 ) ) ;
#12793=DIRECTION ( 'NONE',  ( -0.000000000000000000, -0.000000000000000000, 1.000000000000000000 ) ) ;
#12852=CONICAL_SURFACE ( 'NONE', #31881, 6.500000000000000888, 0.8987552595851582282 ) ;
#12854=PLANE ( 'NONE',  #7818 ) ;
#12870=EDGE_CURVE ( 'NONE', #25544, #866, #16924, .T. ) ;
#12899=CARTESIAN_POINT ( 'NONE',  ( 6.500000000000301981, 0.6542365398607151716, -6.055391205186719361 ) ) ;
#12964=CARTESIAN_POINT ( 'NONE',  ( 8.542937654374687995, 0.000000000000000000, -6.800000000000000711 ) ) ;
#12972=DIRECTION ( 'NONE',  ( 1.000000000000000000, 0.000000000000000000, 0.000000000000000000 ) ) ;
#13032=ORIENTED_EDGE ( 'NONE', *, *, #16789, .T. ) ;
#13073=EDGE_CURVE ( 'NONE', #5826, #734, #252, .T. ) ;
#13087=DIRECTION ( 'NONE',  ( -0.000000000000000000, -0.000000000000000000, 1.000000000000000000 ) ) ;
#13090=CARTESIAN_POINT ( 'NONE',  ( 6.270061300899935297, -4.268872906156509828, -6.443866470201760954 ) ) ;
#13104=ORIENTED_EDGE ( 'NONE', *, *, #25390, .F. ) ;
#13113=ORIENTED_EDGE ( 'NONE', *, *, #20401, .T. ) ;
#13206=FACE_OUTER_BOUND ( 'NONE', #5469, .T. ) ;
#13246=CARTESIAN_POINT ( 'NONE',  ( -6.746558653881498557, 3.895127454924315558, -6.526045885145518533 ) ) ;
#13315=EDGE_CURVE ( 'NONE', #29143, #320, #13320, .T. ) ;
#13320=B_SPLINE_CURVE_WITH_KNOTS ( 'NONE', 3,
 ( #5736, #32134, #16460, #8152, #29416 ),
 .UNSPECIFIED., .F., .F.,
 ( 4, 1, 4 ),
 ( 0.000000000000000000, 0.003752776749732568765, 0.007505553499465137529 ),
 .UNSPECIFIED. ) ;
#13355=CARTESIAN_POINT ( 'NONE',  ( -8.331345277524542681, 1.033251829022860324E-15, -8.000000000000000000 ) ) ;
#13379=B_SPLINE_CURVE_WITH_KNOTS ( 'NONE', 3,
 ( #27932, #7156, #14988, #25377, #1535, #1875, #27761, #4764 ),
 .UNSPECIFIED., .F., .F.,
 ( 4, 2, 2, 4 ),
 ( 2.459764730720142121E-07, 0.001920659145285718043, 0.002880865729692040113, 0.003841072314098362400 ),
 .UNSPECIFIED. ) ;
#13403=ADVANCED_FACE ( 'NONE', ( #23803 ), #25028, .F. ) ;
#13408=CARTESIAN_POINT ( 'NONE',  ( -6.500000000000000000, 3.752776749732564809, -6.064240316920399110 ) ) ;
#13463=VERTEX_POINT ( 'NONE', #803 ) ;
#13465=CARTESIAN_POINT ( 'NONE',  ( 3.999999999999999112, 4.898587196589411843E-16, -7.974599999999998801 ) ) ;
#13517=EDGE_LOOP ( 'NONE', ( #8248, #14890, #29991, #30272, #12521 ) ) ;
#13520=CIRCLE ( 'NONE', #22771, 3.399999999999999911 ) ;
#13537=CARTESIAN_POINT ( 'NONE',  ( -6.499999999999424460, 2.723853875611551789, -6.224027332484248554 ) ) ;
#13567=CIRCLE ( 'NONE', #27723, 4.000000000000000000 ) ;
#13571=CARTESIAN_POINT ( 'NONE',  ( 0.000000000000000000, 0.000000000000000000, -8.000000000000000000 ) ) ;
#13580=CARTESIAN_POINT ( 'NONE',  ( -4.444974277457898637, 4.939246403833854160, -5.720331885005371930 ) ) ;
#13599=CARTESIAN_POINT ( 'NONE',  ( 0.000000000000000000, 0.000000000000000000, 0.000000000000000000 ) ) ;
#13617=DIRECTION ( 'NONE',  ( 1.000000000000000000, 0.000000000000000000, 0.000000000000000000 ) ) ;
#13637=CARTESIAN_POINT ( 'NONE',  ( -6.781345014477444977, -3.590342129888860256, -6.122077150241852728 ) ) ;
#13638=ORIENTED_EDGE ( 'NONE', *, *, #1406, .T. ) ;
#13648=DIRECTION ( 'NONE',  ( 0.000000000000000000, 0.000000000000000000, 1.000000000000000000 ) ) ;
#13688=CARTESIAN_POINT ( 'NONE',  ( -6.270061300899934409, 4.268872906156499170, -6.443866470201760954 ) ) ;
#13788=CARTESIAN_POINT ( 'NONE',  ( -2.971071886220377323, -5.790204346174079753, -4.679857033580009373E-15 ) ) ;
#13792=CARTESIAN_POINT ( 'NONE',  ( -3.339999999999998970, 4.090320309152158050E-16, -0.4621369752184044666 ) ) ;
#13804=CONICAL_SURFACE ( 'NONE', #17601, 8.542937654374687995, 1.221730476396047926 ) ;
#13826=B_SPLINE_CURVE_WITH_KNOTS ( 'NONE', 3,
 ( #8620, #31787, #18349, #6053, #949, #21066 ),
 .UNSPECIFIED., .F., .F.,
 ( 4, 2, 4 ),
 ( 0.003841072314098351557, 0.005765657563962180328, 0.007690242813826009098 ),
 .UNSPECIFIED. ) ;
#13867=ADVANCED_FACE ( 'NONE', ( #9819 ), #10989, .T. ) ;
#13873=B_SPLINE_CURVE_WITH_KNOTS ( 'NONE', 3,
 ( #10543, #13246, #23144, #20420, #7648, #13408 ),
 .UNSPECIFIED., .F., .F.,
 ( 4, 2, 4 ),
 ( -4.604908129294308270E-06, 0.0003318387708545208841, 0.0006682824498383361459 ),
 .UNSPECIFIED. ) ;
#13910=LINE ( 'NONE', #5735, #30950 ) ;
#13972=ORIENTED_EDGE ( 'NONE', *, *, #9785, .T. ) ;
#13982=ORIENTED_EDGE ( 'NONE', *, *, #29106, .T. ) ;
#14024=AXIS2_PLACEMENT_3D ( 'NONE', #28198, #7247, #30931 ) ;
#14051=CARTESIAN_POINT ( 'NONE',  ( -5.441945782601304238, -4.363644636964928658, -0.3576316571898465746 ) ) ;
#14055=CARTESIAN_POINT ( 'NONE',  ( -1.604619215278546562E-14, -7.505553499465138501, -0.8000000000000003775 ) ) ;
#14060=ADVANCED_FACE ( 'NONE', ( #27984 ), #29489, .F. ) ;
#14064=FACE_OUTER_BOUND ( 'NONE', #2977, .T. ) ;
#14107=ORIENTED_EDGE ( 'NONE', *, *, #17375, .F. ) ;
#14150=ORIENTED_EDGE ( 'NONE', *, *, #17436, .T. ) ;
#14168=CARTESIAN_POINT ( 'NONE',  ( 6.837824896291514243, -3.947820044545437224, -6.564402953523717166 ) ) ;
#14224=CARTESIAN_POINT ( 'NONE',  ( -6.500000000000000000, -3.752776749732572803, -6.064240316920399998 ) ) ;
#14254=CARTESIAN_POINT ( 'NONE',  ( 8.542937654374687995, 1.046208125374536008E-15, -6.800000000000000711 ) ) ;
#14261=ORIENTED_EDGE ( 'NONE', *, *, #28028, .F. ) ;
#14268=CARTESIAN_POINT ( 'NONE',  ( -5.699988423468465015, -4.591578518468254266, -6.344710093416085606 ) ) ;
#14270=( NAMED_UNIT ( * ) PLANE_ANGLE_UNIT ( ) SI_UNIT ( $, .RADIAN. ) );
#14274=DIRECTION ( 'NONE',  ( 0.5000000000000006661, 0.8660254037844383745, -0.000000000000000000 ) ) ;
#14367=ORIENTED_EDGE ( 'NONE', *, *, #28754, .F. ) ;
#14400=CARTESIAN_POINT ( 'NONE',  ( 2.141486166123590884, -6.269165884987830673, -0.07763482564821427845 ) ) ;
#14438=FACE_OUTER_BOUND ( 'NONE', #20866, .T. ) ;
#14575=AXIS2_PLACEMENT_3D ( 'NONE', #25907, #2410, #23186 ) ;
#14580=CARTESIAN_POINT ( 'NONE',  ( 6.746887896521486461, 3.895317543251989534, -6.526184258131364935 ) ) ;
#14628=CARTESIAN_POINT ( 'NONE',  ( -3.250000000000004441, 5.629165124598849879, 0.000000000000000000 ) ) ;
#14678=EDGE_LOOP ( 'NONE', ( #27216, #24799, #6219, #6392 ) ) ;
#14707=CARTESIAN_POINT ( 'NONE',  ( 0.000000000000000000, 0.000000000000000000, -8.000000000000000000 ) ) ;
#14726=EDGE_CURVE ( 'NONE', #895, #615, #152, .T. ) ;
#14763=ORIENTED_EDGE ( 'NONE', *, *, #3681, .F. ) ;
#14778=DIRECTION ( 'NONE',  ( 0.000000000000000000, 0.000000000000000000, -1.000000000000000000 ) ) ;
#14779=CARTESIAN_POINT ( 'NONE',  ( 4.424031367840750129, -4.951337798339555007, -6.056431503347240231 ) ) ;
#14814=ORIENTED_EDGE ( 'NONE', *, *, #20351, .T. ) ;
#14823=DIRECTION ( 'NONE',  ( -0.000000000000000000, -0.000000000000000000, 1.000000000000000000 ) ) ;
#14847=APPLICATION_CONTEXT ( 'automotive_design' ) ;
#14890=ORIENTED_EDGE ( 'NONE', *, *, #23368, .T. ) ;
#14921=CARTESIAN_POINT ( 'NONE',  ( -6.500000000000000000, -3.752776749732573247, -0.8000000000000003775 ) ) ;
#14945=EDGE_CURVE ( 'NONE', #10227, #27344, #237, .T. ) ;
#14948=CARTESIAN_POINT ( 'NONE',  ( 6.499999999999999112, -3.752776749732576356, -0.8000000000000003775 ) ) ;
#14955=FACE_OUTER_BOUND ( 'NONE', #3915, .T. ) ;
#14971=B_SPLINE_CURVE_WITH_KNOTS ( 'NONE', 3,
 ( #26642, #13688, #24601, #1262, #24088, #11657, #22040, #19486, #27654, #12158 ),
 .UNSPECIFIED., .F., .F.,
 ( 4, 2, 2, 2, 4 ),
 ( 0.000000000000000000, 0.001989602278884364858, 0.003979204557768729715, 0.005968806836653094139, 0.007958409115537459430 ),
 .UNSPECIFIED. ) ;
#14986=ORIENTED_EDGE ( 'NONE', *, *, #19919, .F. ) ;
#14988=CARTESIAN_POINT ( 'NONE',  ( 1.049032378833991030, 6.899894373156697291, -0.3607371497494544221 ) ) ;
#14989=VERTEX_POINT ( 'NONE', #11862 ) ;
#14994=EDGE_LOOP ( 'NONE', ( #4493, #20807, #17620, #3205 ) ) ;
#15096=CARTESIAN_POINT ( 'NONE',  ( -6.500000000000000888, 0.6470732608156811727, -0.01945970098673090176 ) ) ;
#15121=CARTESIAN_POINT ( 'NONE',  ( 6.781345014477444089, -3.590342129888862921, -6.122077150241852728 ) ) ;
#15135=EDGE_CURVE ( 'NONE', #320, #21727, #11632, .T. ) ;
#15173=EDGE_CURVE ( 'NONE', #20186, #16641, #4184, .T. ) ;
#15180=FACE_BOUND ( 'NONE', #1039, .T. ) ;
#15240=CARTESIAN_POINT ( 'NONE',  ( 6.781345014477444977, 3.590342129888852263, -6.122077150241850951 ) ) ;
#15253=SURFACE_STYLE_FILL_AREA ( #28377 ) ;
#15283=CARTESIAN_POINT ( 'NONE',  ( 6.499999999999398703, -1.392325603688425284, -6.058577540042510812 ) ) ;
#15326=CARTESIAN_POINT ( 'NONE',  ( 3.250000000000004441, 5.629165124598849879, 0.000000000000000000 ) ) ;
#15334=DIRECTION ( 'NONE',  ( 1.000000000000000000, 0.000000000000000000, 0.000000000000000000 ) ) ;
#15375=VERTEX_POINT ( 'NONE', #32607 ) ;
#15458=CARTESIAN_POINT ( 'NONE',  ( 6.500000000000000888, -2.759515168581564204, -5.880113447610522570 ) ) ;
#15465=DIRECTION ( 'NONE',  ( 1.000000000000000000, 0.000000000000000000, 0.000000000000000000 ) ) ;
#15480=CARTESIAN_POINT ( 'NONE',  ( 3.983107665916332252, -5.570601890521292177, -6.171481112545254000 ) ) ;
#15553=LINE ( 'NONE', #64, #6379 ) ;
#15570=CARTESIAN_POINT ( 'NONE',  ( -6.500000000000000000, -3.752776749732572803, -8.000000000000000000 ) ) ;
#15579=DIRECTION ( 'NONE',  ( 0.000000000000000000, 0.000000000000000000, -1.000000000000000000 ) ) ;
#15615=CARTESIAN_POINT ( 'NONE',  ( 6.500000000000000888, -4.076778466486154606, -6.121917890101376436 ) ) ;
#15647=CIRCLE ( 'NONE', #6939, 8.331345277524542681 ) ;
#15664=CIRCLE ( 'NONE', #30908, 3.999999999999999112 ) ;
#15686=DIRECTION ( 'NONE',  ( -1.000000000000000000, 0.000000000000000000, 0.000000000000000000 ) ) ;
#15696=ADVANCED_BREP_SHAPE_REPRESENTATION ( '', ( #951, #2404 ), #27385 ) ;
#15728=ORIENTED_EDGE ( 'NONE', *, *, #23368, .F. ) ;
#15743=ORIENTED_EDGE ( 'NONE', *, *, #13073, .T. ) ;
#15841=AXIS2_PLACEMENT_3D ( 'NONE', #7310, #10539, #26033 ) ;
#15862=EDGE_LOOP ( 'NONE', ( #25499, #30679, #5056, #27093 ) ) ;
#15864=EDGE_LOOP ( 'NONE', ( #26960, #18465, #24924 ) ) ;
#15903=DIRECTION ( 'NONE',  ( -0.5000000000000006661, -0.8660254037844382635, 0.000000000000000000 ) ) ;
#15924=CARTESIAN_POINT ( 'NONE',  ( -6.500000000000000888, -2.727365451017189635, -5.874157743775032969 ) ) ;
#15986=ORIENTED_EDGE ( 'NONE', *, *, #4938, .T. ) ;
#16047=EDGE_CURVE ( 'NONE', #14989, #25544, #26290, .T. ) ;
#16067=CARTESIAN_POINT ( 'NONE',  ( 6.499999999999999112, -1.280811194704859490, -0.07768058122908397256 ) ) ;
#16166=MECHANICAL_DESIGN_GEOMETRIC_PRESENTATION_REPRESENTATION('',(#5310),#6370);
#16355=CARTESIAN_POINT ( 'NONE',  ( 0.04050535873993867109, -7.919512791578240396, -6.573129608219095310 ) ) ;
#16460=CARTESIAN_POINT ( 'NONE',  ( 6.500000000000001776, -5.204170427930421283E-15, -5.592027715088708995 ) ) ;
#16485=CARTESIAN_POINT ( 'NONE',  ( -6.837824896291514243, 3.947820044545427454, -6.564402953523716278 ) ) ;
#16548=CARTESIAN_POINT ( 'NONE',  ( -6.500000000000000000, 3.752776749732564809, -6.064240316920399110 ) ) ;
#16569=B_SPLINE_CURVE_WITH_KNOTS ( 'NONE', 3,
 ( #9421, #19815, #27642, #32586, #30209, #2102 ),
 .UNSPECIFIED., .F., .F.,
 ( 4, 2, 4 ),
 ( 8.673617379884035472E-19, 0.0003352299596252163519, 0.0006704599192504318364 ),
 .UNSPECIFIED. ) ;
#16629=CARTESIAN_POINT ( 'NONE',  ( -4.574783636564603739, 5.228990388888020036, -6.171384342982724647 ) ) ;
#16641=VERTEX_POINT ( 'NONE', #20975 ) ;
#16689=CARTESIAN_POINT ( 'NONE',  ( 3.811597179862312057, -5.304926841629219680, -0.01956314070068839589 ) ) ;
#16789=EDGE_CURVE ( 'NONE', #22659, #7757, #3077, .T. ) ;
#16796=AXIS2_PLACEMENT_3D ( 'NONE', #9894, #14823, #1886 ) ;
#16842=CARTESIAN_POINT ( 'NONE',  ( -4.639619758716985842, 4.826867782832376719, -0.1499059597315285375 ) ) ;
#16924=B_SPLINE_CURVE_WITH_KNOTS ( 'NONE', 3,
 ( #29800, #22458, #22295, #16842, #19573, #32850, #9513, #14628 ),
 .UNSPECIFIED., .F., .F.,
 ( 4, 2, 2, 4 ),
 ( 2.459764730722484167E-07, 0.001920659145285713056, 0.002880865729692032307, 0.003841072314098351557 ),
 .UNSPECIFIED. ) ;
#16927=ORIENTED_EDGE ( 'NONE', *, *, #11754, .T. ) ;
#16962=CARTESIAN_POINT ( 'NONE',  ( -6.500000000000000888, 0.000000000000000000, 0.000000000000000000 ) ) ;
#16977=EDGE_LOOP ( 'NONE', ( #5446, #9781, #14107 ) ) ;
#16985=EDGE_LOOP ( 'NONE', ( #7701, #23243, #10933, #3866, #14150, #4167, #12219 ) ) ;
#16991=PRESENTATION_STYLE_ASSIGNMENT (( #27222 ) ) ;
#17033=ADVANCED_FACE ( 'NONE', ( #20721 ), #31120, .T. ) ;
#17069=B_SPLINE_CURVE_WITH_KNOTS ( 'NONE', 3,
 ( #17202, #17714, #20099, #27586, #19598, #4256, #2048, #12436, #30322, #22827 ),
 .UNSPECIFIED., .F., .F.,
 ( 4, 2, 2, 2, 4 ),
 ( 8.662740229329108052E-20, 0.001989602278884365725, 0.003979204557768730582, 0.005968806836653095874, 0.007958409115537461165 ),
 .UNSPECIFIED. ) ;
#17091=DIRECTION ( 'NONE',  ( 1.000000000000000000, 0.000000000000000000, 0.000000000000000000 ) ) ;
#17123=CARTESIAN_POINT ( 'NONE',  ( 0.5219667817988800085, -7.204195837485521281, -0.5602453477493418710 ) ) ;
#17169=CARTESIAN_POINT ( 'NONE',  ( 1.098735407079012738, -7.248058225758961193, -6.326622577870306685 ) ) ;
#17196=CARTESIAN_POINT ( 'NONE',  ( 3.250000000000003109, -5.629165124598849879, 0.000000000000000000 ) ) ;
#17198=SHAPE_REPRESENTATION ( 'hex flange nut gradea_iso_ISO - 4161 - M8 - N', ( #2404 ), #27385 ) ;
#17202=CARTESIAN_POINT ( 'NONE',  ( -1.269541193505925744E-15, 7.895640089090863789, -6.564402953523717166 ) ) ;
#17236=CARTESIAN_POINT ( 'NONE',  ( 0.000000000000000000, 0.000000000000000000, -25.03750572909317285 ) ) ;
#17321=CARTESIAN_POINT ( 'NONE',  ( -6.500000000000000000, 2.536640449112271156, -0.3753468889000206032 ) ) ;
#17375=EDGE_CURVE ( 'NONE', #8324, #10227, #28836, .T. ) ;
#17397=FACE_OUTER_BOUND ( 'NONE', #9608, .T. ) ;
#17436=EDGE_CURVE ( 'NONE', #20186, #20607, #12596, .T. ) ;
#17483=DIRECTION ( 'NONE',  ( -1.000000000000000000, 0.000000000000000000, 0.000000000000000000 ) ) ;
#17495=VERTEX_POINT ( 'NONE', #6555 ) ;
#17497=CARTESIAN_POINT ( 'NONE',  ( 6.500000000000001776, -4.012858516023013244, -6.470130706010830401 ) ) ;
#17547=ORIENTED_EDGE ( 'NONE', *, *, #299, .F. ) ;
#17568=VECTOR ( 'NONE', #6285, 999.9999999999998863 ) ;
#17600=CARTESIAN_POINT ( 'NONE',  ( 6.500000000000000000, 3.149025070564758888, -0.5705737632551094451 ) ) ;
#17601=AXIS2_PLACEMENT_3D ( 'NONE', #32894, #20286, #7177 ) ;
#17620=ORIENTED_EDGE ( 'NONE', *, *, #2897, .T. ) ;
#17623=CARTESIAN_POINT ( 'NONE',  ( -6.500000000000000000, -3.752776749732573247, -0.8000000000000003775 ) ) ;
#17682=FACE_OUTER_BOUND ( 'NONE', #14678, .T. ) ;
#17702=VERTEX_POINT ( 'NONE', #23241 ) ;
#17714=CARTESIAN_POINT ( 'NONE',  ( 0.5619217318086654478, 7.564468822943301696, -6.443866470201762731 ) ) ;
#17726=LINE ( 'NONE', #4773, #19530 ) ;
#17791=ORIENTED_EDGE ( 'NONE', *, *, #24726, .F. ) ;
#17806=DIRECTION ( 'NONE',  ( -1.000000000000000000, 0.000000000000000000, 0.000000000000000000 ) ) ;
#17840=CARTESIAN_POINT ( 'NONE',  ( 6.500000000000000888, 2.679956093905413450, -6.238387772031967593 ) ) ;
#17851=CARTESIAN_POINT ( 'NONE',  ( 5.589124336234546853, -4.278671059401403021, -6.219623095963592974 ) ) ;
#17973=CARTESIAN_POINT ( 'NONE',  ( 4.444974277457895973, 4.939246403833855936, -5.720331885005371042 ) ) ;
#17989=EDGE_CURVE ( 'NONE', #25974, #5826, #26795, .T. ) ;
#17992=AXIS2_PLACEMENT_3D ( 'NONE', #26548, #18731, #5764 ) ;
#18022=DIRECTION ( 'NONE',  ( -0.000000000000000000, -0.000000000000000000, 1.000000000000000000 ) ) ;
#18076=PLANE ( 'NONE',  #14575 ) ;
#18100=AXIS2_PLACEMENT_3D ( 'NONE', #8123, #18506, #28890 ) ;
#18140=VERTEX_POINT ( 'NONE', #31899 ) ;
#18207=CARTESIAN_POINT ( 'NONE',  ( 3.783380760145018981E-16, -7.895640089090872671, -6.564402953523720718 ) ) ;
#18240=PRODUCT_CONTEXT ( 'NONE', #28141, 'mechanical' ) ;
#18299=VERTEX_POINT ( 'NONE', #18833 ) ;
#18312=CARTESIAN_POINT ( 'NONE',  ( 0.000000000000000000, 0.000000000000000000, -7.554475477074173106 ) ) ;
#18328=EDGE_CURVE ( 'NONE', #6680, #17702, #6477, .T. ) ;
#18349=CARTESIAN_POINT ( 'NONE',  ( -2.141486166123589996, 6.269165884987821791, -0.07763482564820804732 ) ) ;
#18355=ORIENTED_EDGE ( 'NONE', *, *, #26058, .T. ) ;
#18371=CARTESIAN_POINT ( 'NONE',  ( -5.357619327558936585E-16, 7.505553499465137612, -6.064240316920400886 ) ) ;
#18434=VERTEX_POINT ( 'NONE', #14224 ) ;
#18465=ORIENTED_EDGE ( 'NONE', *, *, #19971, .F. ) ;
#18483=FACE_OUTER_BOUND ( 'NONE', #6126, .T. ) ;
#18506=DIRECTION ( 'NONE',  ( -1.000000000000000000, 0.000000000000000000, 0.000000000000000000 ) ) ;
#18511=ORIENTED_EDGE ( 'NONE', *, *, #17989, .T. ) ;
#18526=DIRECTION ( 'NONE',  ( 0.8191520442889923537, 0.000000000000000000, 0.5735764363510453823 ) ) ;
#18547=CARTESIAN_POINT ( 'NONE',  ( 3.783380760145018981E-16, -7.895640089090872671, -6.564402953523720718 ) ) ;
#18674=CARTESIAN_POINT ( 'NONE',  ( -3.999999999999999112, 0.000000000000000000, -7.974599999999998801 ) ) ;
#18676=ADVANCED_FACE ( 'NONE', ( #1957 ), #22841, .F. ) ;
#18731=DIRECTION ( 'NONE',  ( -0.000000000000000000, -0.000000000000000000, 1.000000000000000000 ) ) ;
#18755=ADVANCED_FACE ( 'NONE', ( #7241 ), #12854, .T. ) ;
#18765=ORIENTED_EDGE ( 'NONE', *, *, #16047, .T. ) ;
#18833=CARTESIAN_POINT ( 'NONE',  ( 6.837824896291514243, -3.947820044545437224, -6.564402953523717166 ) ) ;
#18923=CARTESIAN_POINT ( 'NONE',  ( 0.2813450144774466422, -7.667988119308859041, -6.122077150241856280 ) ) ;
#18944=CARTESIAN_POINT ( 'NONE',  ( -5.357619327558936585E-16, 7.505553499465137612, -6.064240316920400886 ) ) ;
#18980=PRODUCT_DEFINITION ( 'UNKNOWN', '', #11028, #29865 ) ;
#19045=B_SPLINE_CURVE_WITH_KNOTS ( 'NONE', 3,
 ( #29673, #22005, #11282, #3270, #8395, #14168 ),
 .UNSPECIFIED., .F., .F.,
 ( 4, 2, 4 ),
 ( 0.003981881017442818506, 0.005970145066490139402, 0.007958409115537461165 ),
 .UNSPECIFIED. ) ;
#19070=CARTESIAN_POINT ( 'NONE',  ( -2.133938722758560669, -6.273523403446323421, -0.09463688534107154993 ) ) ;
#19148=CARTESIAN_POINT ( 'NONE',  ( -6.500000000000000888, 1.416734669062281959, -5.722373386996368438 ) ) ;
#19193=CARTESIAN_POINT ( 'NONE',  ( 0.04050535873994059316, 7.919512791578233291, -6.573129608219092646 ) ) ;
#19215=CARTESIAN_POINT ( 'NONE',  ( -6.500000000000000000, 3.752776749732564809, -0.7999999999999969358 ) ) ;
#19260=CARTESIAN_POINT ( 'NONE',  ( -5.589124336235484769, -4.278671059406953248, -6.219623095964403880 ) ) ;
#19276=AXIS2_PLACEMENT_3D ( 'NONE', #19399, #13087, #7314 ) ;
#19298=EDGE_CURVE ( 'NONE', #734, #13463, #11751, .T. ) ;
#19322=CARTESIAN_POINT ( 'NONE',  ( -6.838249472399978046, -3.995156693690920413, -6.573189567101943354 ) ) ;
#19328=EDGE_LOOP ( 'NONE', ( #32625, #14986, #1688 ) ) ;
#19336=VERTEX_POINT ( 'NONE', #4124 ) ;
#19349=DIRECTION ( 'NONE',  ( -1.000000000000000000, 0.000000000000000000, 0.000000000000000000 ) ) ;
#19399=CARTESIAN_POINT ( 'NONE',  ( 0.000000000000000000, 0.000000000000000000, 0.000000000000000000 ) ) ;
#19459=ORIENTED_EDGE ( 'NONE', *, *, #11754, .F. ) ;
#19486=CARTESIAN_POINT ( 'NONE',  ( -1.126429428730189031, 7.232124035235028892, -6.344710093416086494 ) ) ;
#19523=DIRECTION ( 'NONE',  ( 0.000000000000000000, 0.000000000000000000, 1.000000000000000000 ) ) ;
#19530=VECTOR ( 'NONE', #4094, 1000.000000000000227 ) ;
#19556=DIRECTION ( 'NONE',  ( -0.000000000000000000, -0.000000000000000000, 1.000000000000000000 ) ) ;
#19573=CARTESIAN_POINT ( 'NONE',  ( -4.366061277241453098, 4.984806845751379889, -0.09463688534106590167 ) ) ;
#19598=CARTESIAN_POINT ( 'NONE',  ( 2.832728918602883006, 6.234773369952725020, -6.171481112545252223 ) ) ;
#19607=CARTESIAN_POINT ( 'NONE',  ( 0.000000000000000000, 0.000000000000000000, -8.000000000000000000 ) ) ;
#19720=DIRECTION ( 'NONE',  ( 0.5000000000000005551, -0.8660254037844383745, 0.000000000000000000 ) ) ;
#19757=AXIS2_PLACEMENT_3D ( 'NONE', #5294, #30698, #15686 ) ;
#19763=AXIS2_PLACEMENT_3D ( 'NONE', #13571, #23961, #29242 ) ;
#19766=DIRECTION ( 'NONE',  ( 1.224646799147353207E-16, 1.000000000000000000, 0.000000000000000000 ) ) ;
#19779=ADVANCED_FACE ( 'NONE', ( #21643 ), #8903, .F. ) ;
#19815=CARTESIAN_POINT ( 'NONE',  ( -3.379472811782915531E-16, -7.505553499465146494, -6.177805531628540514 ) ) ;
#19843=CARTESIAN_POINT ( 'NONE',  ( 5.589124336233334489, 4.278671059407959554, -6.219623095966918314 ) ) ;
#19852=FACE_OUTER_BOUND ( 'NONE', #5070, .T. ) ;
#19889=CARTESIAN_POINT ( 'NONE',  ( 5.619193549421182432, -4.261310591078213861, -5.875704392892080463 ) ) ;
#19903=CARTESIAN_POINT ( 'NONE',  ( 6.663127973346137267, -3.846958729056325410, -6.460793508093413351 ) ) ;
#19919=EDGE_CURVE ( 'NONE', #19336, #734, #13379, .T. ) ;
#19941=CARTESIAN_POINT ( 'NONE',  ( -6.831979103402614051, -3.295157223185839701, -6.443785395948805395 ) ) ;
#19958=ORIENTED_EDGE ( 'NONE', *, *, #17375, .T. ) ;
#19971=EDGE_CURVE ( 'NONE', #866, #27344, #8396, .T. ) ;
#19975=AXIS2_PLACEMENT_3D ( 'NONE', #22237, #21895, #6400 ) ;
#19981=EDGE_CURVE ( 'NONE', #22066, #21727, #17069, .T. ) ;
#19995=COLOUR_RGB ( '', 0.40784314, 0.44705882, 0.49803922) ;
#20018=EDGE_CURVE ( 'NONE', #27344, #8324, #25787, .T. ) ;
#20031=CARTESIAN_POINT ( 'NONE',  ( 6.499999999999999112, 3.752776749732563477, -6.177805531628536961 ) ) ;
#20061=FILL_AREA_STYLE ('',( #9328 ) ) ;
#20064=CARTESIAN_POINT ( 'NONE',  ( 6.500000000000000000, 3.752776749732563921, -8.000000000000000000 ) ) ;
#20065=CONICAL_SURFACE ( 'NONE', #16796, 3.339999999999998970, 0.9599310885968821427 ) ;
#20099=CARTESIAN_POINT ( 'NONE',  ( 1.127757440534757238, 7.231345287187090243, -6.344532336093706704 ) ) ;
#20104=EDGE_CURVE ( 'NONE', #16641, #4891, #26863, .T. ) ;
#20119=CARTESIAN_POINT ( 'NONE',  ( -5.357619327558936585E-16, 7.505553499465137612, -6.064240316920400886 ) ) ;
#20173=CIRCLE ( 'NONE', #17992, 3.999999999999999112 ) ;
#20175=CARTESIAN_POINT ( 'NONE',  ( -6.831985876597697072, 3.295913427296342402, -6.443925148804115821 ) ) ;
#20180=CARTESIAN_POINT ( 'NONE',  ( 6.878751942472531411, 3.924677726130922473, -6.573129608219089981 ) ) ;
#20186=VERTEX_POINT ( 'NONE', #2387 ) ;
#20193=( NAMED_UNIT ( * ) SI_UNIT ( $, .STERADIAN. ) SOLID_ANGLE_UNIT ( ) );
#20226=CARTESIAN_POINT ( 'NONE',  ( -2.262848203703084593, -6.566616684922157887, -6.208169345099794789 ) ) ;
#20258=VECTOR ( 'NONE', #531, 1000.000000000000227 ) ;
#20262=ORIENTED_EDGE ( 'NONE', *, *, #29945, .F. ) ;
#20274=CARTESIAN_POINT ( 'NONE',  ( 6.500000000000000000, -3.752776749732574135, -6.064240316920400886 ) ) ;
#20281=CARTESIAN_POINT ( 'NONE',  ( -6.815830331203685866, -1.210827632163352847E-13, -6.171384342982610960 ) ) ;
#20286=DIRECTION ( 'NONE',  ( 0.000000000000000000, 0.000000000000000000, -1.000000000000000000 ) ) ;
#20351=EDGE_CURVE ( 'NONE', #7757, #24155, #7842, .T. ) ;
#20372=( NAMED_UNIT ( * ) PLANE_ANGLE_UNIT ( ) SI_UNIT ( $, .RADIAN. ) );
#20379=DIRECTION ( 'NONE',  ( 0.000000000000000000, 0.000000000000000000, -1.000000000000000000 ) ) ;
#20388=CARTESIAN_POINT ( 'NONE',  ( -1.269541193505925744E-15, 7.895640089090863789, -6.564402953523717166 ) ) ;
#20401=EDGE_CURVE ( 'NONE', #30922, #18140, #26335, .T. ) ;
#20403=CARTESIAN_POINT ( 'NONE',  ( 6.500000000000000888, 1.355443906731431669, -5.756734754743127347 ) ) ;
#20420=CARTESIAN_POINT ( 'NONE',  ( -6.539196172009840602, 3.775406670193650172, -6.286444963328100322 ) ) ;
#20424=CARTESIAN_POINT ( 'NONE',  ( 6.500000000000000000, -3.752776749732574135, -6.064240316920400886 ) ) ;
#20436=ORIENTED_EDGE ( 'NONE', *, *, #15135, .F. ) ;
#20514=CIRCLE ( 'NONE', #29744, 0.6186547224754559426 ) ;
#20539=EDGE_CURVE ( 'NONE', #734, #866, #3494, .T. ) ;
#20554=CONICAL_SURFACE ( 'NONE', #11846, 6.500000000000000888, 0.8987552595851582282 ) ;
#20563=ORIENTED_EDGE ( 'NONE', *, *, #14726, .F. ) ;
#20570=CARTESIAN_POINT ( 'NONE',  ( 6.832273232158034837, 3.329759989367264694, -6.449140625371624580 ) ) ;
#20577=FACE_OUTER_BOUND ( 'NONE', #30356, .T. ) ;
#20607=VERTEX_POINT ( 'NONE', #16485 ) ;
#20611=EDGE_CURVE ( 'NONE', #23539, #8526, #4028, .T. ) ;
#20615=CARTESIAN_POINT ( 'NONE',  ( 6.815830331203685866, 1.228021141713631082E-13, -6.171384342982610960 ) ) ;
#20721=FACE_OUTER_BOUND ( 'NONE', #13517, .T. ) ;
#20759=AXIS2_PLACEMENT_3D ( 'NONE', #28514, #4999, #31237 ) ;
#20771=EDGE_CURVE ( 'NONE', #4891, #16641, #24163, .T. ) ;
#20782=B_SPLINE_CURVE_WITH_KNOTS ( 'NONE', 3,
 ( #18944, #32058, #883, #3779, #16548 ),
 .UNSPECIFIED., .F., .F.,
 ( 4, 1, 4 ),
 ( 0.000000000000000000, 0.003752776749732567897, 0.007505553499465135794 ),
 .UNSPECIFIED. ) ;
#20802=EDGE_LOOP ( 'NONE', ( #17547, #9743, #32609, #21640 ) ) ;
#20807=ORIENTED_EDGE ( 'NONE', *, *, #32365, .T. ) ;
#20834=FACE_OUTER_BOUND ( 'NONE', #16985, .T. ) ;
#20866=EDGE_LOOP ( 'NONE', ( #4454, #3756, #12628, #27686, #27539 ) ) ;
#20944=DIRECTION ( 'NONE',  ( -0.000000000000000000, -0.000000000000000000, 1.000000000000000000 ) ) ;
#20962=LINE ( 'NONE', #10420, #4461 ) ;
#20975=CARTESIAN_POINT ( 'NONE',  ( -8.542937654374687995, 1.046208125374536008E-15, -6.800000000000000711 ) ) ;
#21025=CARTESIAN_POINT ( 'NONE',  ( 6.500000000000000888, 0.000000000000000000, 0.000000000000000000 ) ) ;
#21027=ORIENTED_EDGE ( 'NONE', *, *, #4303, .T. ) ;
#21044=CARTESIAN_POINT ( 'NONE',  ( -6.663120783604270514, -3.846954578056921648, -6.460786012259833733 ) ) ;
#21049=CONICAL_SURFACE ( 'NONE', #19975, 3.999999999999999112, 0.9599310885968813656 ) ;
#21066=CARTESIAN_POINT ( 'NONE',  ( -4.336808689942017736E-16, 7.505553499465137612, -0.8000000000000003775 ) ) ;
#21107=CARTESIAN_POINT ( 'NONE',  ( -3.999999999999999112, 4.898587196589411843E-16, 3.469446951953614189E-15 ) ) ;
#21170=ORIENTED_EDGE ( 'NONE', *, *, #12098, .F. ) ;
#21179=CARTESIAN_POINT ( 'NONE',  ( 6.500000000000000888, -2.534234941938116936, -0.3584823952106179212 ) ) ;
#21210=CARTESIAN_POINT ( 'NONE',  ( -6.500000000000000000, -3.752776749732572803, -6.064240316920399998 ) ) ;
#21244=DIRECTION ( 'NONE',  ( 1.000000000000000000, 0.000000000000000000, 0.000000000000000000 ) ) ;
#21290=CARTESIAN_POINT ( 'NONE',  ( 0.000000000000000000, 0.000000000000000000, 0.000000000000000000 ) ) ;
#21356=DIRECTION ( 'NONE',  ( -0.000000000000000000, -0.000000000000000000, 1.000000000000000000 ) ) ;
#21378=CONICAL_SURFACE ( 'NONE', #19757, 3.999999999999999112, 0.9599310885968813656 ) ;
#21480=CARTESIAN_POINT ( 'NONE',  ( -5.727634848076946561, -4.575561887448768239, -6.326622577870699260 ) ) ;
#21541=EDGE_LOOP ( 'NONE', ( #20563, #11669 ) ) ;
#21549=ORIENTED_EDGE ( 'NONE', *, *, #3474, .T. ) ;
#21572=CARTESIAN_POINT ( 'NONE',  ( -4.424031367838696660, 4.951337798339958240, -6.056431503346038525 ) ) ;
#21604=EDGE_CURVE ( 'NONE', #5932, #5597, #15647, .T. ) ;
#21608=AXIS2_PLACEMENT_3D ( 'NONE', #7639, #18022, #15465 ) ;
#21640=ORIENTED_EDGE ( 'NONE', *, *, #25017, .F. ) ;
#21643=FACE_OUTER_BOUND ( 'NONE', #22272, .T. ) ;
#21722=ORIENTED_EDGE ( 'NONE', *, *, #17436, .F. ) ;
#21727=VERTEX_POINT ( 'NONE', #26976 ) ;
#21813=EDGE_LOOP ( 'NONE', ( #18511, #24069, #1823 ) ) ;
#21842=CARTESIAN_POINT ( 'NONE',  ( 6.499999999999999112, -3.752776749732576356, -0.8000000000000003775 ) ) ;
#21895=DIRECTION ( 'NONE',  ( 0.000000000000000000, 0.000000000000000000, -1.000000000000000000 ) ) ;
#21900=DIRECTION ( 'NONE',  ( 0.000000000000000000, 0.000000000000000000, -1.000000000000000000 ) ) ;
#21901=( NAMED_UNIT ( * ) PLANE_ANGLE_UNIT ( ) SI_UNIT ( $, .RADIAN. ) );
#21934=CONICAL_SURFACE ( 'NONE', #30665, 6.500000000000000888, 0.8987552595851582282 ) ;
#21943=DIRECTION ( 'NONE',  ( -0.8660254037844382635, 0.5000000000000005551, 0.000000000000000000 ) ) ;
#21964=AXIS2_PLACEMENT_3D ( 'NONE', #18312, #21356, #10978 ) ;
#21984=EDGE_CURVE ( 'NONE', #17495, #30922, #33281, .T. ) ;
#22005=CARTESIAN_POINT ( 'NONE',  ( 6.815830331203684089, -0.6610623347507956771, -6.171384342982605631 ) ) ;
#22015=DIRECTION ( 'NONE',  ( -0.000000000000000000, -0.000000000000000000, 1.000000000000000000 ) ) ;
#22026=EDGE_CURVE ( 'NONE', #15375, #4891, #3697, .T. ) ;
#22040=CARTESIAN_POINT ( 'NONE',  ( -2.263183130831070589, 6.566419505188274996, -6.208110906918258287 ) ) ;
#22066=VERTEX_POINT ( 'NONE', #20388 ) ;
#22078=EDGE_CURVE ( 'NONE', #27344, #25544, #10238, .T. ) ;
#22113=CARTESIAN_POINT ( 'NONE',  ( 4.000000000000000000, 0.000000000000000000, -25.03750572909317285 ) ) ;
#22143=ORIENTED_EDGE ( 'NONE', *, *, #24249, .T. ) ;
#22146=DIRECTION ( 'NONE',  ( -1.000000000000000000, 1.224646799147354686E-16, 0.000000000000000000 ) ) ;
#22237=CARTESIAN_POINT ( 'NONE',  ( 0.000000000000000000, 0.000000000000000000, -7.974599999999998801 ) ) ;
#22239=ADVANCED_FACE ( 'NONE', ( #32814 ), #12852, .T. ) ;
#22240=DIRECTION ( 'NONE',  ( 1.000000000000000000, 0.000000000000000000, 0.000000000000000000 ) ) ;
#22265=B_SPLINE_CURVE_WITH_KNOTS ( 'NONE', 3,
 ( #678, #1174, #3393, #521, #19070, #8507, #13788, #11571 ),
 .UNSPECIFIED., .F., .F.,
 ( 4, 2, 2, 4 ),
 ( 2.459764730912720885E-07, 0.001920659145285728234, 0.002880865729692047052, 0.003841072314098365435 ),
 .UNSPECIFIED. ) ;
#22269=ORIENTED_EDGE ( 'NONE', *, *, #6479, .T. ) ;
#22272=EDGE_LOOP ( 'NONE', ( #20262, #24276, #21170, #3208 ) ) ;
#22273=EDGE_CURVE ( 'NONE', #6680, #5826, #2520, .T. ) ;
#22280=CARTESIAN_POINT ( 'NONE',  ( -3.755786496842903988E-16, -7.505553499465146494, -8.000000000000000000 ) ) ;
#22295=CARTESIAN_POINT ( 'NONE',  ( -5.450967621166011412, 4.358435876041001578, -0.3607371497494529233 ) ) ;
#22310=CARTESIAN_POINT ( 'NONE',  ( 5.979512004945807924, -4.053280633787082365, -0.5609245978742287697 ) ) ;
#22311=ORIENTED_EDGE ( 'NONE', *, *, #20104, .F. ) ;
#22315=DIRECTION ( 'NONE',  ( 1.000000000000000000, 0.000000000000000000, 0.000000000000000000 ) ) ;
#22328=CARTESIAN_POINT ( 'NONE',  ( -6.837824896291515131, -3.947820044545435447, -6.564402953523717166 ) ) ;
#22446=DIRECTION ( 'NONE',  ( -1.000000000000000000, 0.000000000000000000, 0.000000000000000000 ) ) ;
#22458=CARTESIAN_POINT ( 'NONE',  ( -5.979512004945809700, 4.053280633787070819, -0.5609245978742248839 ) ) ;
#22523=ADVANCED_FACE ( 'NONE', ( #27461 ), #30362, .F. ) ;
#22547=CARTESIAN_POINT ( 'NONE',  ( 6.499999999999997335, 1.286902272306391870, -0.09436334093186085625 ) ) ;
#22617=CARTESIAN_POINT ( 'NONE',  ( 4.574783636564889733, -5.228990388888015595, -6.171384342982775273 ) ) ;
#22659=VERTEX_POINT ( 'NONE', #9748 ) ;
#22674=CARTESIAN_POINT ( 'NONE',  ( -5.357619327558936585E-16, 7.505553499465138501, -6.177802698399433190 ) ) ;
#22761=CARTESIAN_POINT ( 'NONE',  ( 6.837824896291514243, 3.947820044545427454, -6.564402953523716278 ) ) ;
#22771=AXIS2_PLACEMENT_3D ( 'NONE', #28940, #8172, #26383 ) ;
#22788=CARTESIAN_POINT ( 'NONE',  ( 6.815964470354069604, -1.383691465878164717, -6.173460172893482145 ) ) ;
#22797=CARTESIAN_POINT ( 'NONE',  ( 6.878751942472530523, -3.924677726130933575, -6.573129608219091757 ) ) ;
#22827=CARTESIAN_POINT ( 'NONE',  ( 6.837824896291514243, 3.947820044545427454, -6.564402953523716278 ) ) ;
#22830=CARTESIAN_POINT ( 'NONE',  ( -8.331345277524542681, 1.020295532671184640E-15, -7.381345277524544279 ) ) ;
#22835=CARTESIAN_POINT ( 'NONE',  ( 3.250000000000001332, -5.629165124598862313, -5.592027715088713435 ) ) ;
#22840=CARTESIAN_POINT ( 'NONE',  ( -6.815830331203685866, -0.6619522098568484392, -6.171384342982615401 ) ) ;
#22841=( BOUNDED_SURFACE ( )  B_SPLINE_SURFACE ( 3, 2, ( 
 ( #15240, #12179, #20180 ),
 ( #4680, #19843, #28192 ),
 ( #17973, #12520, #4850 ),
 ( #27839, #1779, #22908 ),
 ( #33302, #4509, #25631 ),
 ( #24962, #30239, #5020 ) ),
 .UNSPECIFIED., .F., .F., .T. ) 
 B_SPLINE_SURFACE_WITH_KNOTS ( ( 4, 2, 4 ),
 ( 3, 3 ),
 ( 0.003190620565844220352, 0.007281897438794486706, 0.01137317431174475306 ),
 ( 0.000000000000000000, 1.000000000000000000 ),
 .UNSPECIFIED. ) 
 GEOMETRIC_REPRESENTATION_ITEM ( )  RATIONAL_B_SPLINE_SURFACE ( (
 ( 1.000000000000000000, 0.8047731410850402778, 1.000000000000000000),
 ( 1.000000000000000000, 0.8125552299142427826, 1.000000000000000000),
 ( 1.000000000000000000, 0.8191520442908248878, 1.000000000000000000),
 ( 1.000000000000000000, 0.8191520442871482732, 1.000000000000000000),
 ( 1.000000000000000000, 0.8125552299170040182, 1.000000000000000000),
 ( 1.000000000000000000, 0.8047731410850399447, 1.000000000000000000) ) ) 
 REPRESENTATION_ITEM ( '' )  SURFACE ( )  );
#22908=CARTESIAN_POINT ( 'NONE',  ( 2.241046694639346804, 6.576374040526301812, -6.171384342982712212 ) ) ;
#22926=CARTESIAN_POINT ( 'NONE',  ( -6.500000000000000888, 4.012863338656273982, -6.470131626772281486 ) ) ;
#22937=DIRECTION ( 'NONE',  ( 1.000000000000000000, 0.000000000000000000, 0.000000000000000000 ) ) ;
#23035=CARTESIAN_POINT ( 'NONE',  ( 3.250000000000004441, 5.629165124598849879, 0.000000000000000000 ) ) ;
#23098=EDGE_CURVE ( 'NONE', #25974, #6680, #11780, .T. ) ;
#23111=CARTESIAN_POINT ( 'NONE',  ( 0.000000000000000000, 0.000000000000000000, 0.000000000000000000 ) ) ;
#23144=CARTESIAN_POINT ( 'NONE',  ( -6.663120783604270514, 3.846954578056913654, -6.460786012259833733 ) ) ;
#23186=DIRECTION ( 'NONE',  ( 1.000000000000000000, 0.000000000000000000, -0.000000000000000000 ) ) ;
#23241=CARTESIAN_POINT ( 'NONE',  ( -1.604619215278546562E-14, -7.505553499465138501, -0.8000000000000003775 ) ) ;
#23243=ORIENTED_EDGE ( 'NONE', *, *, #22026, .T. ) ;
#23294=CARTESIAN_POINT ( 'NONE',  ( 6.500000000000000888, 2.723353699433710862, -5.896365680526115760 ) ) ;
#23328=EDGE_CURVE ( 'NONE', #320, #13463, #28608, .T. ) ;
#23337=CARTESIAN_POINT ( 'NONE',  ( 6.818272094961329799, 1.321852500971154365, -6.208027553811807486 ) ) ;
#23368=EDGE_CURVE ( 'NONE', #14989, #18434, #6334, .T. ) ;
#23450=ORIENTED_EDGE ( 'NONE', *, *, #19298, .F. ) ;
#23465=ORIENTED_EDGE ( 'NONE', *, *, #299, .T. ) ;
#23485=CONICAL_SURFACE ( 'NONE', #20759, 8.542937654374687995, 1.221730476396047926 ) ;
#23539=VERTEX_POINT ( 'NONE', #18547 ) ;
#23644=CARTESIAN_POINT ( 'NONE',  ( -2.055025722542106692, 6.319083845363845597, -5.720331885005371930 ) ) ;
#23668=ORIENTED_EDGE ( 'NONE', *, *, #26407, .F. ) ;
#23768=CARTESIAN_POINT ( 'NONE',  ( -6.746558653882965828, -3.895127454921782029, -6.526045885145518533 ) ) ;
#23771=AXIS2_PLACEMENT_3D ( 'NONE', #9288, #30247, #27185 ) ;
#23803=FACE_OUTER_BOUND ( 'NONE', #7232, .T. ) ;
#23900=B_SPLINE_CURVE_WITH_KNOTS ( 'NONE', 3,
 ( #27910, #9516, #32853, #19903, #33016, #1680 ),
 .UNSPECIFIED., .F., .F.,
 ( 4, 2, 4 ),
 ( 8.673617379884035472E-19, 0.0003352299596252132619, 0.0006704599192504256564 ),
 .UNSPECIFIED. ) ;
#23961=DIRECTION ( 'NONE',  ( 0.000000000000000000, 0.000000000000000000, 1.000000000000000000 ) ) ;
#23971=CARTESIAN_POINT ( 'NONE',  ( 0.2259792476677715822, 7.636022678937395725, -6.470294263593361350 ) ) ;
#24069=ORIENTED_EDGE ( 'NONE', *, *, #22273, .F. ) ;
#24088=CARTESIAN_POINT ( 'NONE',  ( -3.983107665916332252, 5.570601890521282407, -6.171481112545251335 ) ) ;
#24155=VERTEX_POINT ( 'NONE', #18674 ) ;
#24163=CIRCLE ( 'NONE', #6757, 8.542937654374687995 ) ;
#24197=ORIENTED_EDGE ( 'NONE', *, *, #20539, .T. ) ;
#24249=EDGE_CURVE ( 'NONE', #18434, #73, #2081, .T. ) ;
#24255=CARTESIAN_POINT ( 'NONE',  ( -6.500000000000000000, -4.014037567183532218, -6.470355840301004413 ) ) ;
#24271=VERTEX_POINT ( 'NONE', #1287 ) ;
#24276=ORIENTED_EDGE ( 'NONE', *, *, #20611, .F. ) ;
#24285=B_SPLINE_CURVE_WITH_KNOTS ( 'NONE', 3,
 ( #1592, #25433, #6872, #22547, #4481, #7213, #25267, #17600, #27991, #4657 ),
 .UNSPECIFIED., .F., .F.,
 ( 4, 2, 2, 2, 4 ),
 ( 0.009353627468483380336, 0.01031000219096067476, 0.01126637691343796918, 0.01222275163591526534, 0.01317912635839255976 ),
 .UNSPECIFIED. ) ;
#24370=DIRECTION ( 'NONE',  ( 1.000000000000000000, 0.000000000000000000, 0.000000000000000000 ) ) ;
#24372=CARTESIAN_POINT ( 'NONE',  ( -6.878751942472531411, -3.924677726130930910, -6.573129608219091757 ) ) ;
#24373=EDGE_LOOP ( 'NONE', ( #14261, #22143, #6998, #8429, #19958 ) ) ;
#24447=CARTESIAN_POINT ( 'NONE',  ( -5.978033218201117549, -4.054134411712201569, -0.5602453477493345435 ) ) ;
#24472=DIRECTION ( 'NONE',  ( 0.000000000000000000, 0.000000000000000000, 1.000000000000000000 ) ) ;
#24551=CYLINDRICAL_SURFACE ( 'NONE', #29314, 3.399999999999999911 ) ;
#24601=CARTESIAN_POINT ( 'NONE',  ( -5.698650001973517121, 4.592339236403562452, -6.344532336093705815 ) ) ;
#24726=EDGE_CURVE ( 'NONE', #24155, #7757, #15664, .T. ) ;
#24772=DIRECTION ( 'NONE',  ( 1.000000000000000000, 0.000000000000000000, 0.000000000000000000 ) ) ;
#24799=ORIENTED_EDGE ( 'NONE', *, *, #29161, .F. ) ;
#24832=CARTESIAN_POINT ( 'NONE',  ( -4.555094537983154446, -5.243183837310248840, -6.208110906918257399 ) ) ;
#24856=AXIS2_PLACEMENT_3D ( 'NONE', #29829, #31867, #8531 ) ;
#24878=ORIENTED_EDGE ( 'NONE', *, *, #31264, .T. ) ;
#24882=VECTOR ( 'NONE', #65, 1000.000000000000000 ) ;
#24924=ORIENTED_EDGE ( 'NONE', *, *, #12870, .F. ) ;
#24962=CARTESIAN_POINT ( 'NONE',  ( -0.2813450144774468642, 7.667988119308851047, -6.122077150241852728 ) ) ;
#24964=CARTESIAN_POINT ( 'NONE',  ( -3.755786496842903988E-16, -7.505553499465146494, -6.064240316920404439 ) ) ;
#24966=ORIENTED_EDGE ( 'NONE', *, *, #20611, .T. ) ;
#25012=FACE_OUTER_BOUND ( 'NONE', #16977, .T. ) ;
#25017=EDGE_CURVE ( 'NONE', #22659, #18140, #11589, .T. ) ;
#25028=( BOUNDED_SURFACE ( )  B_SPLINE_SURFACE ( 3, 2, ( 
 ( #8796, #23971, #19193 ),
 ( #8467, #26688, #3191 ),
 ( #23644, #31640, #3349 ),
 ( #13580, #21572, #16629 ),
 ( #31485, #5577, #29590 ),
 ( #633, #6241, #11032 ) ),
 .UNSPECIFIED., .F., .F., .T. ) 
 B_SPLINE_SURFACE_WITH_KNOTS ( ( 4, 2, 4 ),
 ( 3, 3 ),
 ( 0.003190620565844218184, 0.007281897438794484971, 0.01137317431174475132 ),
 ( 0.000000000000000000, 1.000000000000000000 ),
 .UNSPECIFIED. ) 
 GEOMETRIC_REPRESENTATION_ITEM ( )  RATIONAL_B_SPLINE_SURFACE ( (
 ( 1.000000000000000000, 0.8047731410850399447, 1.000000000000000000),
 ( 1.000000000000000000, 0.8125552299156222347, 1.000000000000000000),
 ( 1.000000000000000000, 0.8191520442889872466, 1.000000000000000000),
 ( 1.000000000000000000, 0.8191520442889872466, 1.000000000000000000),
 ( 1.000000000000000000, 0.8125552299156223457, 1.000000000000000000),
 ( 1.000000000000000000, 0.8047731410850402778, 1.000000000000000000) ) ) 
 REPRESENTATION_ITEM ( '' )  SURFACE ( )  );
#25040=CARTESIAN_POINT ( 'NONE',  ( 4.366061277241453098, -4.984806845751389659, -0.09463688534107157768 ) ) ;
#25127=CYLINDRICAL_SURFACE ( 'NONE', #26825, 4.000000000000000000 ) ;
#25135=B_SPLINE_CURVE_WITH_KNOTS ( 'NONE', 3,
 ( #22328, #19941, #4777, #33056, #22840, #20281 ),
 .UNSPECIFIED., .F., .F.,
 ( 4, 2, 4 ),
 ( 0.000000000000000000, 0.001990940508721414457, 0.003981881017442828914 ),
 .UNSPECIFIED. ) ;
#25197=EDGE_CURVE ( 'NONE', #21727, #15375, #26791, .T. ) ;
#25200=DIRECTION ( 'NONE',  ( 0.000000000000000000, 0.000000000000000000, 1.000000000000000000 ) ) ;
#25232=CARTESIAN_POINT ( 'NONE',  ( -1.269541193505925744E-15, 7.895640089090863789, -6.564402953523717166 ) ) ;
#25267=CARTESIAN_POINT ( 'NONE',  ( 6.500000000000000888, 2.536640449112275153, -0.3753468889000217690 ) ) ;
#25287=CARTESIAN_POINT ( 'NONE',  ( -6.815830331203685866, -1.210827632163352847E-13, -6.171384342982610960 ) ) ;
#25377=CARTESIAN_POINT ( 'NONE',  ( 1.860380241283018377, 6.431462466365323927, -0.1499059597315287040 ) ) ;
#25390=EDGE_CURVE ( 'NONE', #73, #17702, #8815, .T. ) ;
#25418=AXIS2_PLACEMENT_3D ( 'NONE', #22280, #19720, #6779 ) ;
#25433=CARTESIAN_POINT ( 'NONE',  ( 6.500000000000000888, 0.3213925021621134026, 6.640738306473707756E-16 ) ) ;
#25434=EDGE_CURVE ( 'NONE', #18140, #30922, #13520, .T. ) ;
#25499=ORIENTED_EDGE ( 'NONE', *, *, #16789, .F. ) ;
#25544=VERTEX_POINT ( 'NONE', #19215 ) ;
#25557=ORIENTED_EDGE ( 'NONE', *, *, #22273, .T. ) ;
#25586=ORIENTED_EDGE ( 'NONE', *, *, #25197, .F. ) ;
#25592=CARTESIAN_POINT ( 'NONE',  ( 3.809068165403724393, 5.306386968807659699, 9.757819552369535962E-16 ) ) ;
#25631=CARTESIAN_POINT ( 'NONE',  ( 1.098735407079667992, 7.248058225760153128, -6.326622577870739228 ) ) ;
#25651=CARTESIAN_POINT ( 'NONE',  ( -6.500000000000000888, 2.759383090082417667, -5.880088986491048608 ) ) ;
#25677=CARTESIAN_POINT ( 'NONE',  ( 6.826575449902429149, 2.663085462279306981, -6.347418139105299950 ) ) ;
#25757=ORIENTED_EDGE ( 'NONE', *, *, #24726, .T. ) ;
#25764=ADVANCED_FACE ( 'NONE', ( #14438 ), #11718, .F. ) ;
#25787=CIRCLE ( 'NONE', #2421, 6.500000000000000888 ) ;
#25812=FACE_OUTER_BOUND ( 'NONE', #21813, .T. ) ;
#25852=CARTESIAN_POINT ( 'NONE',  ( 6.500000000000000000, -1.417018949932591365, -5.722407714414702085 ) ) ;
#25887=CARTESIAN_POINT ( 'NONE',  ( 6.826399921716642005, 2.638123634694624631, -6.344399053232583796 ) ) ;
#25907=CARTESIAN_POINT ( 'NONE',  ( -12.99999999999999112, -3.903127820947815962E-15, -8.000000000000000000 ) ) ;
#25959=ORIENTED_EDGE ( 'NONE', *, *, #4798, .T. ) ;
#25974=VERTEX_POINT ( 'NONE', #14948 ) ;
#26017=ADVANCED_FACE ( 'NONE', ( #2003 ), #28525, .F. ) ;
#26033=DIRECTION ( 'NONE',  ( 0.000000000000000000, 0.000000000000000000, -1.000000000000000000 ) ) ;
#26055=EDGE_LOOP ( 'NONE', ( #32031, #5519, #5186, #5785 ) ) ;
#26058=EDGE_CURVE ( 'NONE', #866, #19336, #13826, .T. ) ;
#26062=DIRECTION ( 'NONE',  ( 1.000000000000000000, 0.000000000000000000, 0.000000000000000000 ) ) ;
#26198=CARTESIAN_POINT ( 'NONE',  ( 2.263183130831067924, -6.566419505188284766, -6.208110906918261840 ) ) ;
#26290=LINE ( 'NONE', #29014, #1209 ) ;
#26321=ORIENTED_EDGE ( 'NONE', *, *, #19981, .F. ) ;
#26335=CIRCLE ( 'NONE', #31240, 3.399999999999999911 ) ;
#26383=DIRECTION ( 'NONE',  ( 1.000000000000000000, 0.000000000000000000, 0.000000000000000000 ) ) ;
#26393=DIRECTION ( 'NONE',  ( -0.000000000000000000, -0.000000000000000000, 1.000000000000000000 ) ) ;
#26407=EDGE_CURVE ( 'NONE', #24271, #5394, #30317, .T. ) ;
#26426=ADVANCED_FACE ( 'NONE', ( #14064 ), #21049, .F. ) ;
#26444=ADVANCED_FACE ( 'NONE', ( #8955 ), #3102, .T. ) ;
#26447=ORIENTED_EDGE ( 'NONE', *, *, #26407, .T. ) ;
#26460=CLOSED_SHELL ( 'NONE', ( #33066, #26426, #2190, #4109, #26444, #10877, #1909, #28327, #10424, #25764, #1017, #18755, #17033, #30183, #28541, #10654, #12460, #5572, #33424, #10456, #22239, #1474, #13867, #19779, #31417, #7099, #26017, #13403, #18676, #14060, #32016, #22523 ) ) ;
#26481=CARTESIAN_POINT ( 'NONE',  ( -6.500000000000001776, -2.692912473542373952, -6.218066308278946686 ) ) ;
#26510=FACE_OUTER_BOUND ( 'NONE', #20802, .T. ) ;
#26534=CIRCLE ( 'NONE', #9127, 6.500000000000000888 ) ;
#26548=CARTESIAN_POINT ( 'NONE',  ( 0.000000000000000000, 0.000000000000000000, 3.469446951953614189E-15 ) ) ;
#26594=FACE_OUTER_BOUND ( 'NONE', #6128, .T. ) ;
#26616=DIRECTION ( 'NONE',  ( 0.000000000000000000, 0.000000000000000000, 1.000000000000000000 ) ) ;
#26642=CARTESIAN_POINT ( 'NONE',  ( -6.837824896291514243, 3.947820044545427454, -6.564402953523716278 ) ) ;
#26645=CARTESIAN_POINT ( 'NONE',  ( -6.500000000000000000, 1.392044006191029304, -6.058542048163745086 ) ) ;
#26674=UNCERTAINTY_MEASURE_WITH_UNIT (LENGTH_MEASURE( 1.000000000000000082E-05 ), #27550, 'distance_accuracy_value', 'NONE');
#26688=CARTESIAN_POINT ( 'NONE',  ( -0.9108756637653833144, 6.979659189792688956, -6.219623095965475024 ) ) ;
#26774=ORIENTED_EDGE ( 'NONE', *, *, #4798, .F. ) ;
#26791=B_SPLINE_CURVE_WITH_KNOTS ( 'NONE', 3,
 ( #5266, #5104, #25887, #23337, #31167, #20615 ),
 .UNSPECIFIED., .F., .F.,
 ( 4, 2, 4 ),
 ( 0.000000000000000000, 0.001990940508721409253, 0.003981881017442818506 ),
 .UNSPECIFIED. ) ;
#26795=B_SPLINE_CURVE_WITH_KNOTS ( 'NONE', 3,
 ( #21842, #8899, #21179, #16067, #1234, #32233 ),
 .UNSPECIFIED., .F., .F.,
 ( 4, 2, 4 ),
 ( 0.005511122051665403969, 0.007432374760074392586, 0.009353627468483380336 ),
 .UNSPECIFIED. ) ;
#26803=CARTESIAN_POINT ( 'NONE',  ( -6.500000000000000000, -3.752776749732572803, -6.064240316920399998 ) ) ;
#26825=AXIS2_PLACEMENT_3D ( 'NONE', #33147, #6570, #22240 ) ;
#26854=CARTESIAN_POINT ( 'NONE',  ( 0.000000000000000000, 0.000000000000000000, 3.469446951953614189E-15 ) ) ;
#26863=CIRCLE ( 'NONE', #12747, 8.542937654374687995 ) ;
#26925=CARTESIAN_POINT ( 'NONE',  ( -4.444974277458378253, -4.939246403833585042, -5.720331885005373707 ) ) ;
#26960=ORIENTED_EDGE ( 'NONE', *, *, #22078, .F. ) ;
#26976=CARTESIAN_POINT ( 'NONE',  ( 6.837824896291514243, 3.947820044545427454, -6.564402953523716278 ) ) ;
#26996=CARTESIAN_POINT ( 'NONE',  ( -3.250000000000003997, -5.629165124598849879, 0.000000000000000000 ) ) ;
#27075=AXIS2_PLACEMENT_3D ( 'NONE', #7180, #6838, #30009 ) ;
#27093=ORIENTED_EDGE ( 'NONE', *, *, #20351, .F. ) ;
#27097=CARTESIAN_POINT ( 'NONE',  ( -4.574783636564919931, -5.228990388887469365, -6.171384342982607407 ) ) ;
#27158=DIRECTION ( 'NONE',  ( -0.000000000000000000, -0.000000000000000000, 1.000000000000000000 ) ) ;
#27177=CARTESIAN_POINT ( 'NONE',  ( 1.058054217398695762, -6.894685612232789751, -0.3576316571898509600 ) ) ;
#27185=DIRECTION ( 'NONE',  ( 1.000000000000000000, 0.000000000000000000, 0.000000000000000000 ) ) ;
#27216=ORIENTED_EDGE ( 'NONE', *, *, #12098, .T. ) ;
#27220=CARTESIAN_POINT ( 'NONE',  ( -2.832728918602883006, -6.234773369952733901, -6.171481112545254000 ) ) ;
#27222=SURFACE_STYLE_USAGE ( .BOTH. , #30460 ) ;
#27279=FACE_OUTER_BOUND ( 'NONE', #3084, .T. ) ;
#27288=ORIENTED_EDGE ( 'NONE', *, *, #23098, .T. ) ;
#27344=VERTEX_POINT ( 'NONE', #8756 ) ;
#27345=DIRECTION ( 'NONE',  ( 1.000000000000000000, 0.000000000000000000, 0.000000000000000000 ) ) ;
#27379=ORIENTED_EDGE ( 'NONE', *, *, #33469, .F. ) ;
#27385=( GEOMETRIC_REPRESENTATION_CONTEXT ( 3 ) GLOBAL_UNCERTAINTY_ASSIGNED_CONTEXT ( ( #5552 ) ) GLOBAL_UNIT_ASSIGNED_CONTEXT ( ( #29579, #21901, #11692 ) ) REPRESENTATION_CONTEXT ( 'NONE', 'WORKASPACE' ) );
#27428=DIRECTION ( 'NONE',  ( 1.000000000000000000, 0.000000000000000000, 0.000000000000000000 ) ) ;
#27461=FACE_OUTER_BOUND ( 'NONE', #3581, .T. ) ;
#27539=ORIENTED_EDGE ( 'NONE', *, *, #17989, .F. ) ;
#27550=( LENGTH_UNIT ( ) NAMED_UNIT ( * ) SI_UNIT ( .MILLI., .METRE. ) );
#27586=CARTESIAN_POINT ( 'NONE',  ( 2.262848203703083261, 6.566616684922145453, -6.208169345099790348 ) ) ;
#27629=EDGE_CURVE ( 'NONE', #20607, #22066, #14971, .T. ) ;
#27642=CARTESIAN_POINT ( 'NONE',  ( -2.654873707089686533E-16, -7.550815748621508838, -6.286450516130496879 ) ) ;
#27654=CARTESIAN_POINT ( 'NONE',  ( -0.5620262070071414540, 7.564407249984292037, -6.443844059477446429 ) ) ;
#27686=ORIENTED_EDGE ( 'NONE', *, *, #11152, .F. ) ;
#27723=AXIS2_PLACEMENT_3D ( 'NONE', #28310, #33068, #12972 ) ;
#27761=CARTESIAN_POINT ( 'NONE',  ( 2.971071886220372438, 5.790204346174072647, 1.063026348804146728E-15 ) ) ;
#27819=CARTESIAN_POINT ( 'NONE',  ( -3.399999999999999911, 4.163799117101000559E-16, -8.000000000000000000 ) ) ;
#27839=CARTESIAN_POINT ( 'NONE',  ( 2.055025722542103583, 6.319083845363847374, -5.720331885005371042 ) ) ;
#27845=ORIENTED_EDGE ( 'NONE', *, *, #6402, .T. ) ;
#27859=DIRECTION ( 'NONE',  ( -1.000000000000000000, 0.000000000000000000, 0.000000000000000000 ) ) ;
#27869=CARTESIAN_POINT ( 'NONE',  ( -6.500000000000000000, 3.453380256388206782, -0.6809028088495794329 ) ) ;
#27887=DIRECTION ( 'NONE',  ( 1.000000000000000000, 0.000000000000000000, 0.000000000000000000 ) ) ;
#27896=CARTESIAN_POINT ( 'NONE',  ( 2.241046694638796133, -6.576374040525796438, -6.171384342982452864 ) ) ;
#27910=CARTESIAN_POINT ( 'NONE',  ( 6.500000000000000000, -3.752776749732574135, -6.064240316920400886 ) ) ;
#27932=CARTESIAN_POINT ( 'NONE',  ( -4.336808689942017736E-16, 7.505553499465137612, -0.8000000000000003775 ) ) ;
#27984=FACE_OUTER_BOUND ( 'NONE', #4040, .T. ) ;
#27991=CARTESIAN_POINT ( 'NONE',  ( 6.500000000000000000, 3.453380256388213887, -0.6809028088495826525 ) ) ;
#28028=EDGE_CURVE ( 'NONE', #18434, #10227, #15553, .T. ) ;
#28029=FILL_AREA_STYLE_COLOUR ( '', #31744 ) ;
#28033=EDGE_CURVE ( 'NONE', #15375, #18299, #19045, .T. ) ;
#28069=CARTESIAN_POINT ( 'NONE',  ( -0.2259792476677704443, -7.636022678937404606, -6.470294263593365791 ) ) ;
#28101=VECTOR ( 'NONE', #18526, 999.9999999999998863 ) ;
#28141=APPLICATION_CONTEXT ( 'automotive_design' ) ;
#28192=CARTESIAN_POINT ( 'NONE',  ( 5.727634848076855967, 4.575561887447700649, -6.326622577870477215 ) ) ;
#28198=CARTESIAN_POINT ( 'NONE',  ( 0.000000000000000000, 0.000000000000000000, 0.000000000000000000 ) ) ;
#28211=CARTESIAN_POINT ( 'NONE',  ( -6.838238953609876880, 3.993985489099932007, -6.572971244646267586 ) ) ;
#28218=PRODUCT_DEFINITION_SHAPE ( 'NONE', 'NONE',  #18980 ) ;
#28310=CARTESIAN_POINT ( 'NONE',  ( 0.000000000000000000, 0.000000000000000000, -8.000000000000000000 ) ) ;
#28327=ADVANCED_FACE ( 'NONE', ( #17397 ), #30515, .T. ) ;
#28372=( BOUNDED_SURFACE ( )  B_SPLINE_SURFACE ( 3, 2, ( 
 ( #2153, #22926, #28211 ),
 ( #25651, #13537, #32098 ),
 ( #19148, #26645, #8760 ),
 ( #11159, #29381, #29210 ),
 ( #15924, #26481, #8595 ),
 ( #593, #24255, #19322 ) ),
 .UNSPECIFIED., .F., .F., .T. ) 
 B_SPLINE_SURFACE_WITH_KNOTS ( ( 4, 2, 4 ),
 ( 3, 3 ),
 ( 0.03172058138205611361, 0.03571597378202086281, 0.03971136618198560508 ),
 ( 0.000000000000000000, 1.000000000000000000 ),
 .UNSPECIFIED. ) 
 GEOMETRIC_REPRESENTATION_ITEM ( )  RATIONAL_B_SPLINE_SURFACE ( (
 ( 1.000000000000000000, 0.8047780791350982454, 1.000000000000000000),
 ( 1.000000000000000000, 0.8123796029720318224, 1.000000000000000000),
 ( 1.000000000000000000, 0.8190681660673523323, 1.000000000000000000),
 ( 1.000000000000000000, 0.8192342536572917444, 1.000000000000000000),
 ( 1.000000000000000000, 0.8126124427164184150, 1.000000000000000000),
 ( 1.000000000000000000, 0.8047712715942066941, 1.000000000000000000) ) ) 
 REPRESENTATION_ITEM ( '' )  SURFACE ( )  );
#28377=FILL_AREA_STYLE ('',( #28029 ) ) ;
#28393=CARTESIAN_POINT ( 'NONE',  ( -6.499999999999999112, 2.227636940139124722, -0.2900584647821222717 ) ) ;
#28429=CARTESIAN_POINT ( 'NONE',  ( 6.837824896291514243, -3.947820044545437224, -6.564402953523717166 ) ) ;
#28514=CARTESIAN_POINT ( 'NONE',  ( 0.000000000000000000, 0.000000000000000000, -6.800000000000000711 ) ) ;
#28525=( BOUNDED_SURFACE ( )  B_SPLINE_SURFACE ( 3, 2, ( 
 ( #15615, #17497, #33350 ),
 ( #15458, #12394, #10361 ),
 ( #25852, #15283, #22788 ),
 ( #33181, #12899, #2513 ),
 ( #20403, #30796, #2346 ),
 ( #23294, #17840, #25677 ),
 ( #12736, #10187, #20570 ),
 ( #29235, #10683, #3505 ) ),
 .UNSPECIFIED., .F., .F., .T. ) 
 B_SPLINE_SURFACE_WITH_KNOTS ( ( 4, 2, 2, 4 ),
 ( 3, 3 ),
 ( 0.03170918191602133812, 0.03570420671717101924, 0.03770171911774586326, 0.03969923151832070729 ),
 ( 0.000000000000000000, 1.000000000000000000 ),
 .UNSPECIFIED. ) 
 GEOMETRIC_REPRESENTATION_ITEM ( )  RATIONAL_B_SPLINE_SURFACE ( (
 ( 1.000000000000000000, 0.8047781070930550840, 1.000000000000000000),
 ( 1.000000000000000000, 0.8123787894255611874, 1.000000000000000000),
 ( 1.000000000000000000, 0.8190667557154468481, 1.000000000000000000),
 ( 1.000000000000000000, 0.8191933945820784047, 1.000000000000000000),
 ( 1.000000000000000000, 0.8176087340369108114, 1.000000000000000000),
 ( 1.000000000000000000, 0.8122956952719621038, 1.000000000000000000),
 ( 1.000000000000000000, 0.8086308540103167575, 1.000000000000000000),
 ( 1.000000000000000000, 0.8047712493762134711, 1.000000000000000000) ) ) 
 REPRESENTATION_ITEM ( '' )  SURFACE ( )  );
#28541=ADVANCED_FACE ( 'NONE', ( #15180, #5128 ), #18076, .F. ) ;
#28577=ORIENTED_EDGE ( 'NONE', *, *, #3681, .T. ) ;
#28598=CARTESIAN_POINT ( 'NONE',  ( 4.555432764205793461, -5.242992371775935467, -6.208169345099792125 ) ) ;
#28608=LINE ( 'NONE', #2549, #33572 ) ;
#28613=ORIENTED_EDGE ( 'NONE', *, *, #15135, .T. ) ;
#28638=FACE_OUTER_BOUND ( 'NONE', #15862, .T. ) ;
#28754=EDGE_CURVE ( 'NONE', #8324, #6680, #26534, .T. ) ;
#28780=ORIENTED_EDGE ( 'NONE', *, *, #18328, .F. ) ;
#28836=B_SPLINE_CURVE_WITH_KNOTS ( 'NONE', 3,
 ( #26996, #3657, #1111, #14051, #24447, #17623 ),
 .UNSPECIFIED., .F., .F.,
 ( 4, 2, 4 ),
 ( 0.003841072314098365435, 0.005765657563962188134, 0.007690242813826009965 ),
 .UNSPECIFIED. ) ;
#28844=EDGE_CURVE ( 'NONE', #17702, #8324, #22265, .T. ) ;
#28847=CARTESIAN_POINT ( 'NONE',  ( 3.999999999999999112, 4.898587196589411843E-16, -7.974599999999998801 ) ) ;
#28890=DIRECTION ( 'NONE',  ( 0.000000000000000000, 0.000000000000000000, 1.000000000000000000 ) ) ;
#28940=CARTESIAN_POINT ( 'NONE',  ( 0.000000000000000000, 0.000000000000000000, -0.4201245229258211977 ) ) ;
#28943=( BOUNDED_SURFACE ( )  B_SPLINE_SURFACE ( 3, 2, ( 
 ( #6783, #28069, #4393 ),
 ( #4569, #10032, #17169 ),
 ( #12400, #2012, #27896 ),
 ( #9503, #14779, #22617 ),
 ( #19889, #17851, #4732 ),
 ( #15121, #12059, #22797 ) ),
 .UNSPECIFIED., .F., .F., .T. ) 
 B_SPLINE_SURFACE_WITH_KNOTS ( ( 4, 2, 4 ),
 ( 3, 3 ),
 ( 0.003190620565844226857, 0.007281897438794493645, 0.01137317431174476000 ),
 ( 0.000000000000000000, 1.000000000000000000 ),
 .UNSPECIFIED. ) 
 GEOMETRIC_REPRESENTATION_ITEM ( )  RATIONAL_B_SPLINE_SURFACE ( (
 ( 1.000000000000000000, 0.8047731410850399447, 1.000000000000000000),
 ( 1.000000000000000000, 0.8125552299147021929, 1.000000000000000000),
 ( 1.000000000000000000, 0.8191520442902128218, 1.000000000000000000),
 ( 1.000000000000000000, 0.8191520442877616714, 1.000000000000000000),
 ( 1.000000000000000000, 0.8125552299165426096, 1.000000000000000000),
 ( 1.000000000000000000, 0.8047731410850402778, 1.000000000000000000) ) ) 
 REPRESENTATION_ITEM ( '' )  SURFACE ( )  );
#29014=CARTESIAN_POINT ( 'NONE',  ( -6.500000000000000000, 3.752776749732564809, -8.000000000000000000 ) ) ;
#29026=( GEOMETRIC_REPRESENTATION_CONTEXT ( 3 ) GLOBAL_UNCERTAINTY_ASSIGNED_CONTEXT ( ( #1240 ) ) GLOBAL_UNIT_ASSIGNED_CONTEXT ( ( #4525, #20372, #20193 ) ) REPRESENTATION_CONTEXT ( 'NONE', 'WORKASPACE' ) );
#29037=CARTESIAN_POINT ( 'NONE',  ( -6.500000000000000000, 3.752776749732564809, -6.064240316920399110 ) ) ;
#29049=B_SPLINE_CURVE_WITH_KNOTS ( 'NONE', 3,
 ( #5570, #29703, #31635, #6539, #1093 ),
 .UNSPECIFIED., .F., .F.,
 ( 4, 1, 4 ),
 ( 0.000000000000000000, 0.003752776749732569198, 0.007505553499465138396 ),
 .UNSPECIFIED. ) ;
#29050=CARTESIAN_POINT ( 'NONE',  ( -6.837824896291515131, -3.947820044545435447, -6.564402953523717166 ) ) ;
#29053=ORIENTED_EDGE ( 'NONE', *, *, #4303, .F. ) ;
#29106=EDGE_CURVE ( 'NONE', #29143, #18299, #23900, .T. ) ;
#29108=DIRECTION ( 'NONE',  ( 1.000000000000000000, 0.000000000000000000, 0.000000000000000000 ) ) ;
#29143=VERTEX_POINT ( 'NONE', #20424 ) ;
#29161=EDGE_CURVE ( 'NONE', #18299, #23539, #9654, .T. ) ;
#29210=CARTESIAN_POINT ( 'NONE',  ( -6.815701034932152069, -1.328907527188669668, -6.169383458210047522 ) ) ;
#29235=CARTESIAN_POINT ( 'NONE',  ( 6.500000000000000888, 4.077976443323007238, -6.122137821720842865 ) ) ;
#29237=VECTOR ( 'NONE', #9647, 1000.000000000000000 ) ;
#29242=DIRECTION ( 'NONE',  ( 1.000000000000000000, 0.000000000000000000, 0.000000000000000000 ) ) ;
#29314=AXIS2_PLACEMENT_3D ( 'NONE', #19607, #13648, #3593 ) ;
#29326=VERTEX_POINT ( 'NONE', #18371 ) ;
#29381=CARTESIAN_POINT ( 'NONE',  ( -6.500000000000000000, -1.336926445777093964, -6.054363369342815382 ) ) ;
#29396=ORIENTED_EDGE ( 'NONE', *, *, #22026, .F. ) ;
#29416=CARTESIAN_POINT ( 'NONE',  ( 6.500000000000000000, 3.752776749732563921, -6.064240316920399110 ) ) ;
#29489=CONICAL_SURFACE ( 'NONE', #33295, 3.339999999999998970, 0.9599310885968821427 ) ;
#29579=( LENGTH_UNIT ( ) NAMED_UNIT ( * ) SI_UNIT ( .MILLI., .METRE. ) );
#29590=CARTESIAN_POINT ( 'NONE',  ( -5.727634848077285845, 4.575561887448583498, -6.326622577870772979 ) ) ;
#29673=CARTESIAN_POINT ( 'NONE',  ( 6.815830331203685866, 1.228021141713631082E-13, -6.171384342982610960 ) ) ;
#29703=CARTESIAN_POINT ( 'NONE',  ( 5.416666666666667851, 4.378239541354659536, -5.848636054922034866 ) ) ;
#29744=AXIS2_PLACEMENT_3D ( 'NONE', #22830, #19766, #22146 ) ;
#29800=CARTESIAN_POINT ( 'NONE',  ( -6.500000000000000000, 3.752776749732564809, -0.7999999999999969358 ) ) ;
#29817=CARTESIAN_POINT ( 'NONE',  ( 3.528928113779637776, -5.468125903023631551, -5.911160594572010107E-15 ) ) ;
#29829=CARTESIAN_POINT ( 'NONE',  ( 0.000000000000000000, 0.000000000000000000, -7.554475477074173106 ) ) ;
#29865=PRODUCT_DEFINITION_CONTEXT ( 'detailed design', #14847, 'design' ) ;
#29919=CARTESIAN_POINT ( 'NONE',  ( 6.500000000000000000, -3.752776749732574135, -8.000000000000000000 ) ) ;
#29945=EDGE_CURVE ( 'NONE', #8526, #18434, #700, .T. ) ;
#29949=CARTESIAN_POINT ( 'NONE',  ( -6.837824896291515131, -3.947820044545435447, -6.564402953523717166 ) ) ;
#29991=ORIENTED_EDGE ( 'NONE', *, *, #28028, .T. ) ;
#30009=DIRECTION ( 'NONE',  ( -0.8660254037844382635, -0.5000000000000006661, 0.000000000000000000 ) ) ;
#30107=EDGE_LOOP ( 'NONE', ( #13982, #1961, #25586, #20436, #12304 ) ) ;
#30183=ADVANCED_FACE ( 'NONE', ( #1904, #4111 ), #9397, .T. ) ;
#30209=CARTESIAN_POINT ( 'NONE',  ( -4.411512144081271877E-13, -7.790635086499372086, -6.526184258131371152 ) ) ;
#30239=CARTESIAN_POINT ( 'NONE',  ( -0.2259792476677698891, 7.636022678937394836, -6.470294263593361350 ) ) ;
#30247=DIRECTION ( 'NONE',  ( -0.000000000000000000, -0.000000000000000000, 1.000000000000000000 ) ) ;
#30266=CARTESIAN_POINT ( 'NONE',  ( 0.000000000000000000, 0.000000000000000000, 0.000000000000000000 ) ) ;
#30272=ORIENTED_EDGE ( 'NONE', *, *, #14945, .T. ) ;
#30282=CARTESIAN_POINT ( 'NONE',  ( -1.127757440534757460, -7.231345287187099125, -6.344532336093708480 ) ) ;
#30283=FACE_OUTER_BOUND ( 'NONE', #3407, .T. ) ;
#30317=CIRCLE ( 'NONE', #31394, 4.000000000000000000 ) ;
#30322=CARTESIAN_POINT ( 'NONE',  ( 6.269955739554010421, 4.268932597852939104, -6.443844059477442876 ) ) ;
#30356=EDGE_LOOP ( 'NONE', ( #32824, #8902, #21549, #22311 ) ) ;
#30362=CYLINDRICAL_SURFACE ( 'NONE', #7428, 4.000000000000000000 ) ;
#30384=CARTESIAN_POINT ( 'NONE',  ( -3.399999999999999911, 4.163799117101000559E-16, -0.4201245229258211977 ) ) ;
#30427=LINE ( 'NONE', #29919, #10767 ) ;
#30431=CARTESIAN_POINT ( 'NONE',  ( 6.539198257601831266, 3.775407874310744649, -6.286450516130488886 ) ) ;
#30460=SURFACE_SIDE_STYLE ('',( #12054 ) ) ;
#30515=PLANE ( 'NONE',  #27075 ) ;
#30573=CARTESIAN_POINT ( 'NONE',  ( -6.837824896291514243, 3.947820044545427454, -6.564402953523716278 ) ) ;
#30593=SHAPE_REPRESENTATION_RELATIONSHIP ( 'NONE' , 'NONE' ,  #17198, #15696 ) ;
#30594=AXIS2_PLACEMENT_3D ( 'NONE', #26854, #3515, #21244 ) ;
#30598=CARTESIAN_POINT ( 'NONE',  ( -6.500000000000000888, -2.534234941938113828, -0.3584823952106175882 ) ) ;
#30611=CARTESIAN_POINT ( 'NONE',  ( -6.500000000000000000, 1.602771114417265164, -0.1495523863686162858 ) ) ;
#30665=AXIS2_PLACEMENT_3D ( 'NONE', #5194, #15579, #17806 ) ;
#30679=ORIENTED_EDGE ( 'NONE', *, *, #33469, .T. ) ;
#30698=DIRECTION ( 'NONE',  ( 0.000000000000000000, 0.000000000000000000, -1.000000000000000000 ) ) ;
#30771=CARTESIAN_POINT ( 'NONE',  ( 0.000000000000000000, 0.000000000000000000, 0.000000000000000000 ) ) ;
#30796=CARTESIAN_POINT ( 'NONE',  ( 6.500000000000000888, 1.333904739168207065, -6.094327662196326933 ) ) ;
#30908=AXIS2_PLACEMENT_3D ( 'NONE', #3085, #32197, #24370 ) ;
#30922=VERTEX_POINT ( 'NONE', #30384 ) ;
#30927=CONICAL_SURFACE ( 'NONE', #14024, 6.500000000000000888, 0.8987552595851582282 ) ;
#30931=DIRECTION ( 'NONE',  ( -1.000000000000000000, 0.000000000000000000, 0.000000000000000000 ) ) ;
#30950=VECTOR ( 'NONE', #24472, 1000.000000000000000 ) ;
#31097=CARTESIAN_POINT ( 'NONE',  ( 8.331345277524542681, 0.000000000000000000, -8.000000000000000000 ) ) ;
#31120=PLANE ( 'NONE',  #18100 ) ;
#31150=CARTESIAN_POINT ( 'NONE',  ( 2.837346585668845567, -6.232092946297389524, -6.171287963165198676 ) ) ;
#31167=CARTESIAN_POINT ( 'NONE',  ( 6.815830331203685866, 0.6619522098568483282, -6.171384342982615401 ) ) ;
#31237=DIRECTION ( 'NONE',  ( -1.000000000000000000, 0.000000000000000000, 0.000000000000000000 ) ) ;
#31240=AXIS2_PLACEMENT_3D ( 'NONE', #3372, #32156, #29108 ) ;
#31264=EDGE_CURVE ( 'NONE', #24271, #7757, #11558, .T. ) ;
#31394=AXIS2_PLACEMENT_3D ( 'NONE', #32790, #32120, #27345 ) ;
#31417=ADVANCED_FACE ( 'NONE', ( #17682 ), #28943, .F. ) ;
#31485=CARTESIAN_POINT ( 'NONE',  ( -5.619193549421041212, 4.261310591078285803, -5.875704392894027350 ) ) ;
#31512=CARTESIAN_POINT ( 'NONE',  ( -6.500000000000000000, -3.752776749732573247, -0.8000000000000003775 ) ) ;
#31632=CARTESIAN_POINT ( 'NONE',  ( 3.339999999999998970, 0.000000000000000000, -0.4621369752184044666 ) ) ;
#31635=CARTESIAN_POINT ( 'NONE',  ( 3.250000000000000444, 5.629165124598851655, -5.592027715088707218 ) ) ;
#31640=CARTESIAN_POINT ( 'NONE',  ( -2.075968632161309557, 6.306992450857741517, -6.056431503346038525 ) ) ;
#31664=DIRECTION ( 'NONE',  ( 0.000000000000000000, 0.000000000000000000, 1.000000000000000000 ) ) ;
#31744=COLOUR_RGB ( '', 0.40784314, 0.44705882, 0.49803922) ;
#31777=AXIS2_PLACEMENT_3D ( 'NONE', #32875, #9368, #27428 ) ;
#31787=CARTESIAN_POINT ( 'NONE',  ( -2.690931834596280936, 5.951943280390038282, 1.006275141338108408E-15 ) ) ;
#31790=EDGE_CURVE ( 'NONE', #18140, #895, #10536, .T. ) ;
#31867=DIRECTION ( 'NONE',  ( -0.000000000000000000, -0.000000000000000000, 1.000000000000000000 ) ) ;
#31881=AXIS2_PLACEMENT_3D ( 'NONE', #30266, #4372, #17483 ) ;
#31899=CARTESIAN_POINT ( 'NONE',  ( 3.399999999999999911, 0.000000000000000000, -0.4201245229258211977 ) ) ;
#31995=VECTOR ( 'NONE', #10892, 1000.000000000000000 ) ;
#32016=ADVANCED_FACE ( 'NONE', ( #28638 ), #21378, .F. ) ;
#32031=ORIENTED_EDGE ( 'NONE', *, *, #2528, .T. ) ;
#32037=CARTESIAN_POINT ( 'NONE',  ( -2.241046694638765935, -6.576374040526340892, -6.171384342982618065 ) ) ;
#32058=CARTESIAN_POINT ( 'NONE',  ( -1.083333333333333259, 6.880090707843040221, -5.848636054922037530 ) ) ;
#32089=CARTESIAN_POINT ( 'NONE',  ( -6.500000000000000000, 2.501851166488374911, -5.848636054922034866 ) ) ;
#32098=CARTESIAN_POINT ( 'NONE',  ( -6.826580258811596025, 2.695816818222440681, -6.331007506863580048 ) ) ;
#32120=DIRECTION ( 'NONE',  ( -0.000000000000000000, -0.000000000000000000, -1.000000000000000000 ) ) ;
#32134=CARTESIAN_POINT ( 'NONE',  ( 6.500000000000000000, -2.501851166488383349, -5.848636054922036642 ) ) ;
#32156=DIRECTION ( 'NONE',  ( 0.000000000000000000, 0.000000000000000000, -1.000000000000000000 ) ) ;
#32197=DIRECTION ( 'NONE',  ( -0.000000000000000000, -0.000000000000000000, 1.000000000000000000 ) ) ;
#32233=CARTESIAN_POINT ( 'NONE',  ( 6.500000000000000888, 0.000000000000000000, 0.000000000000000000 ) ) ;
#32286=CARTESIAN_POINT ( 'NONE',  ( -5.416666666666667851, -4.378239541354669306, -5.848636054922036642 ) ) ;
#32365=EDGE_CURVE ( 'NONE', #30922, #615, #3070, .T. ) ;
#32367=CARTESIAN_POINT ( 'NONE',  ( -4.424031367838992423, -4.951337798339370266, -6.056431503346042078 ) ) ;
#32500=DIRECTION ( 'NONE',  ( -0.000000000000000000, -0.000000000000000000, 1.000000000000000000 ) ) ;
#32586=CARTESIAN_POINT ( 'NONE',  ( -2.654873707089192509E-16, -7.693917458112650820, -6.460793508093416904 ) ) ;
#32607=CARTESIAN_POINT ( 'NONE',  ( 6.815830331203685866, 1.228021141713631082E-13, -6.171384342982610960 ) ) ;
#32609=ORIENTED_EDGE ( 'NONE', *, *, #25434, .F. ) ;
#32625=ORIENTED_EDGE ( 'NONE', *, *, #20539, .F. ) ;
#32661=CARTESIAN_POINT ( 'NONE',  ( -6.269955739554009533, -4.268932597852945321, -6.443844059477445541 ) ) ;
#32712=FACE_OUTER_BOUND ( 'NONE', #14994, .T. ) ;
#32790=CARTESIAN_POINT ( 'NONE',  ( 0.000000000000000000, 0.000000000000000000, -8.000000000000000000 ) ) ;
#32802=DIRECTION ( 'NONE',  ( -0.9396926207859143121, 0.000000000000000000, -0.3420201433256525592 ) ) ;
#32814=FACE_OUTER_BOUND ( 'NONE', #15864, .T. ) ;
#32824=ORIENTED_EDGE ( 'NONE', *, *, #381, .F. ) ;
#32850=CARTESIAN_POINT ( 'NONE',  ( -3.811597179862308060, 5.304926841629211687, -0.01956314070068241109 ) ) ;
#32853=CARTESIAN_POINT ( 'NONE',  ( 6.539198257601831266, -3.775407874310755307, -6.286450516130489774 ) ) ;
#32875=CARTESIAN_POINT ( 'NONE',  ( 0.000000000000000000, 0.000000000000000000, 0.000000000000000000 ) ) ;
#32883=CARTESIAN_POINT ( 'NONE',  ( 5.416666666666667851, -4.378239541354669306, -5.848636054922037530 ) ) ;
#32894=CARTESIAN_POINT ( 'NONE',  ( 0.000000000000000000, 0.000000000000000000, -6.800000000000000711 ) ) ;
#32918=ORIENTED_EDGE ( 'NONE', *, *, #11152, .T. ) ;
#33016=CARTESIAN_POINT ( 'NONE',  ( 6.746887896522740569, -3.895317543249826819, -6.526184258131365823 ) ) ;
#33039=DIRECTION ( 'NONE',  ( 0.000000000000000000, 0.000000000000000000, 1.000000000000000000 ) ) ;
#33056=CARTESIAN_POINT ( 'NONE',  ( -6.818272094961329799, -1.321852500971156363, -6.208027553811807486 ) ) ;
#33066=ADVANCED_FACE ( 'NONE', ( #19852 ), #25127, .F. ) ;
#33068=DIRECTION ( 'NONE',  ( -0.000000000000000000, -0.000000000000000000, -1.000000000000000000 ) ) ;
#33147=CARTESIAN_POINT ( 'NONE',  ( 0.000000000000000000, 0.000000000000000000, -25.03750572909317285 ) ) ;
#33150=SURFACE_SIDE_STYLE ('',( #15253 ) ) ;
#33166=CARTESIAN_POINT ( 'NONE',  ( -6.500000000000000888, 0.000000000000000000, 0.000000000000000000 ) ) ;
#33181=CARTESIAN_POINT ( 'NONE',  ( 6.500000000000000000, 0.6659426636835951152, -5.719325464431898709 ) ) ;
#33186=ORIENTED_EDGE ( 'NONE', *, *, #6402, .F. ) ;
#33281=LINE ( 'NONE', #27819, #24882 ) ;
#33295=AXIS2_PLACEMENT_3D ( 'NONE', #4134, #1585, #17091 ) ;
#33302=CARTESIAN_POINT ( 'NONE',  ( 0.8808064505786590281, 6.997019658119588925, -5.875704392892181716 ) ) ;
#33350=CARTESIAN_POINT ( 'NONE',  ( 6.838238910409970117, -3.993980678889271552, -6.572970348078615466 ) ) ;
#33424=ADVANCED_FACE ( 'NONE', ( #18483 ), #21934, .T. ) ;
#33432=CARTESIAN_POINT ( 'NONE',  ( 4.358513833876415333, 4.989164364209877967, -0.07763482564820642362 ) ) ;
#33469=EDGE_CURVE ( 'NONE', #22659, #17495, #8905, .T. ) ;
#33510=ORIENTED_EDGE ( 'NONE', *, *, #32365, .F. ) ;
#33572=VECTOR ( 'NONE', #25200, 1000.000000000000000 ) ;
ENDSEC;
END-ISO-10303-21;
